ISO-10303-21;
HEADER;
FILE_DESCRIPTION (('STEP AP214'),
    '1' );
FILE_NAME ('hex flange bolt small_iso_ISO 4162 - M5 x 20 x 20-N.step',
    '2026-10-06T08:09:25',
    ( '' ),
    ( '' ),
    'SwSTEP 2.0',
    'SolidWorks 2021',
    '' );
FILE_SCHEMA (( 'AUTOMOTIVE_DESIGN' ));
ENDSEC;

DATA;
#45=DIRECTION ( 'NONE',  ( 5.916456789157585037E-31, -0.4999999999999997224, 0.8660254037844388186 ) ) ;
#69=ADVANCED_FACE ( 'NONE', ( #20975 ), #1306, .T. ) ;
#80=CARTESIAN_POINT ( 'NONE',  ( 3.806834918298653392, 3.031088913245603589, -1.750000000000057065 ) ) ;
#97=CARTESIAN_POINT ( 'NONE',  ( 3.973514160553469843, -2.741076955031381157, -2.383932505289878101 ) ) ;
#115=CIRCLE ( 'NONE', #13253, 5.200000000000008171 ) ;
#120=FACE_OUTER_BOUND ( 'NONE', #16147, .T. ) ;
#123=ORIENTED_EDGE ( 'NONE', *, *, #8630, .F. ) ;
#130=CARTESIAN_POINT ( 'NONE',  ( 4.071447262713884463, 2.020725942163639655, -3.499999999999996003 ) ) ;
#188=CARTESIAN_POINT ( 'NONE',  ( 0.1388410611046271836, 2.351840044243041827, -2.926493552096059769 ) ) ;
#217=EDGE_CURVE ( 'NONE', #19662, #17819, #14141, .T. ) ;
#233=CARTESIAN_POINT ( 'NONE',  ( 4.180231891692635315, -2.049421325483237410, -3.591231015387320813 ) ) ;
#238=CARTESIAN_POINT ( 'NONE',  ( 0.3126073911696378160, 2.020725942163612121, 3.499999999999975131 ) ) ;
#243=CARTESIAN_POINT ( 'NONE',  ( 3.972066048304788932, 2.740530939476398142, -2.384802634787798414 ) ) ;
#275=B_SPLINE_CURVE_WITH_KNOTS ( 'NONE', 3,
 ( #5062, #11991, #17398, #21068, #10229 ),
 .UNSPECIFIED., .F., .F.,
 ( 4, 1, 4 ),
 ( 0.000000000000000000, 0.002020725942163690073, 0.004041451884327380145 ),
 .UNSPECIFIED. ) ;
#285=CARTESIAN_POINT ( 'NONE',  ( 5.600000000000000533, -2.020725942163709377, -3.500000000000010214 ) ) ;
#294=PLANE ( 'NONE',  #19723 ) ;
#296=B_SPLINE_CURVE_WITH_KNOTS ( 'NONE', 3,
 ( #9686, #20518, #6167, #6504, #16841 ),
 .UNSPECIFIED., .F., .F.,
 ( 4, 1, 4 ),
 ( 6.992893892674682497E-18, 0.002020725942163693108, 0.004041451884327379278 ),
 .UNSPECIFIED. ) ;
#304=B_SPLINE_CURVE_WITH_KNOTS ( 'NONE', 3,
 ( #10582, #16334, #21540, #16095, #19528, #238 ),
 .UNSPECIFIED., .F., .F.,
 ( 4, 2, 4 ),
 ( 0.005852013090620712850, 0.006875955131657994837, 0.007899897172695277692 ),
 .UNSPECIFIED. ) ;
#318=EDGE_CURVE ( 'NONE', #5868, #10391, #18968, .T. ) ;
#338=STYLED_ITEM ( 'NONE', ( #9590 ), #11971 ) ;
#352=ADVANCED_FACE ( 'NONE', ( #14705 ), #16571, .T. ) ;
#360=CARTESIAN_POINT ( 'NONE',  ( 4.180345304246198879, 2.049116244671355336, -3.591763845239319242 ) ) ;
#390=CARTESIAN_POINT ( 'NONE',  ( 0.000000000000000000, -3.031088913245480576, 1.749999999999994671 ) ) ;
#411=CARTESIAN_POINT ( 'NONE',  ( 4.175813232069149450, -2.061359961916378492, -3.570380186727402538 ) ) ;
#424=ORIENTED_EDGE ( 'NONE', *, *, #2047, .F. ) ;
#429=VECTOR ( 'NONE', #14345, 1000.000000000000000 ) ;
#432=CARTESIAN_POINT ( 'NONE',  ( 4.175075985190096262, -4.120741555260265088, -6.938893903907228378E-15 ) ) ;
#443=CARTESIAN_POINT ( 'NONE',  ( 4.030859730899538640, -1.403482646610872742, -3.500000000000009770 ) ) ;
#486=CARTESIAN_POINT ( 'NONE',  ( 0.000000000000000000, 0.000000000000000000, 0.000000000000000000 ) ) ;
#488=EDGE_CURVE ( 'NONE', #8317, #12509, #8824, .T. ) ;
#558=FACE_OUTER_BOUND ( 'NONE', #8377, .T. ) ;
#570=CARTESIAN_POINT ( 'NONE',  ( 3.948111298835275562, -0.6968132764965153658, -3.500000000000165645 ) ) ;
#588=LINE ( 'NONE', #7872, #10422 ) ;
#611=EDGE_CURVE ( 'NONE', #9771, #21672, #8198, .T. ) ;
#620=CARTESIAN_POINT ( 'NONE',  ( 4.071447262713884463, -2.020725942163709377, 3.500000000000003109 ) ) ;
#641=ADVANCED_FACE ( 'NONE', ( #120 ), #9980, .F. ) ;
#651=CARTESIAN_POINT ( 'NONE',  ( 0.000000000000000000, 0.000000000000000000, 0.000000000000000000 ) ) ;
#652=B_SPLINE_CURVE_WITH_KNOTS ( 'NONE', 3,
 ( #20311, #7837, #2535, #432, #9723, #15003, #6073, #903, #7602, #16877, #7951, #15112, #4174, #21964, #22307, #6195 ),
 .UNSPECIFIED., .F., .F.,
 ( 4, 3, 3, 3, 3, 4 ),
 ( -2.111273352549518886E-06, 0.000000000000000000, 3.519286887793778349E-05, 7.191842652069384322E-05, 0.0001049868727093698859, 0.0001382836236822112402 ),
 .UNSPECIFIED. ) ;
#655=ORIENTED_EDGE ( 'NONE', *, *, #20733, .T. ) ;
#656=( NAMED_UNIT ( * ) SI_UNIT ( $, .STERADIAN. ) SOLID_ANGLE_UNIT ( ) );
#664=CARTESIAN_POINT ( 'NONE',  ( 4.071447262713884463, -2.020725942163709377, 3.500000000000003109 ) ) ;
#670=DIRECTION ( 'NONE',  ( -1.000000000000000000, -1.479114197289397135E-31, -5.916456789157588541E-31 ) ) ;
#686=ORIENTED_EDGE ( 'NONE', *, *, #1852, .F. ) ;
#716=AXIS2_PLACEMENT_3D ( 'NONE', #8767, #5361, #3594 ) ;
#725=ORIENTED_EDGE ( 'NONE', *, *, #6094, .F. ) ;
#726=CARTESIAN_POINT ( 'NONE',  ( 4.165266963751736995, 4.099263933823925399, 3.718842205176018431E-15 ) ) ;
#771=EDGE_LOOP ( 'NONE', ( #10334, #9517, #6211, #11513, #11978, #14081 ) ) ;
#776=ADVANCED_FACE ( 'NONE', ( #15751 ), #4354, .T. ) ;
#777=ORIENTED_EDGE ( 'NONE', *, *, #17393, .T. ) ;
#847=CARTESIAN_POINT ( 'NONE',  ( 0.000000000000000000, 3.031088913245508110, -1.750000000000029310 ) ) ;
#900=CARTESIAN_POINT ( 'NONE',  ( 4.151274195509679465, -2.039912954708795745, 3.533232880573519363 ) ) ;
#903=CARTESIAN_POINT ( 'NONE',  ( 4.151274195509675913, -4.079825909417513330, -2.794074523180553099E-14 ) ) ;
#921=DIRECTION ( 'NONE',  ( -7.395570986446975166E-31, -3.382522293539642681E-32, -1.000000000000000000 ) ) ;
#927=VERTEX_POINT ( 'NONE', #22218 ) ;
#960=ORIENTED_EDGE ( 'NONE', *, *, #1744, .T. ) ;
#994=CARTESIAN_POINT ( 'NONE',  ( 5.100000000000000533, 6.368163355566246242E-16, -5.200000000000011724 ) ) ;
#1004=VERTEX_POINT ( 'NONE', #20924 ) ;
#1049=CARTESIAN_POINT ( 'NONE',  ( 0.3126073911696378160, -2.020725942163709377, 3.500000000000003109 ) ) ;
#1052=CARTESIAN_POINT ( 'NONE',  ( 4.030867648404781178, 3.732851566701672841, 0.5345114293579794618 ) ) ;
#1134=CARTESIAN_POINT ( 'NONE',  ( 4.104070371397483541, -2.023683613428362005, 3.505122836902511807 ) ) ;
#1140=DIRECTION ( 'NONE',  ( 0.000000000000000000, 3.382522293539642133E-32, 1.000000000000000000 ) ) ;
#1178=VERTEX_POINT ( 'NONE', #9026 ) ;
#1212=ORIENTED_EDGE ( 'NONE', *, *, #318, .T. ) ;
#1217=AXIS2_PLACEMENT_3D ( 'NONE', #8285, #6518, #15441 ) ;
#1298=CARTESIAN_POINT ( 'NONE',  ( 5.600000000000000533, 4.041451884327335264, -1.734723475976807094E-14 ) ) ;
#1299=EDGE_LOOP ( 'NONE', ( #4669, #13365, #960, #3584 ) ) ;
#1306=CONICAL_SURFACE ( 'NONE', #14454, 3.500000000000004441, 1.047197551196600296 ) ;
#1330=VERTEX_POINT ( 'NONE', #19844 ) ;
#1347=EDGE_CURVE ( 'NONE', #5868, #17819, #1969, .T. ) ;
#1353=ORIENTED_EDGE ( 'NONE', *, *, #11369, .T. ) ;
#1375=AXIS2_PLACEMENT_3D ( 'NONE', #1590, #4999, #20901 ) ;
#1381=CARTESIAN_POINT ( 'NONE',  ( 4.630153689607049650, 0.000000000000000000, -3.469446951953614189E-15 ) ) ;
#1403=CONICAL_SURFACE ( 'NONE', #9662, 5.371010071662839280, 1.221730476396037490 ) ;
#1404=DIRECTION ( 'NONE',  ( 1.000000000000000000, 1.479114197289397135E-31, -7.395570986446975166E-31 ) ) ;
#1434=ORIENTED_EDGE ( 'NONE', *, *, #488, .F. ) ;
#1459=ORIENTED_EDGE ( 'NONE', *, *, #2823, .F. ) ;
#1475=CARTESIAN_POINT ( 'NONE',  ( 4.071447262713884463, -2.020725942163709377, 3.500000000000003109 ) ) ;
#1485=EDGE_CURVE ( 'NONE', #13386, #1178, #9993, .T. ) ;
#1493=EDGE_LOOP ( 'NONE', ( #12083, #18786, #20478, #1434 ) ) ;
#1505=ORIENTED_EDGE ( 'NONE', *, *, #611, .T. ) ;
#1571=VERTEX_POINT ( 'NONE', #7326 ) ;
#1590=CARTESIAN_POINT ( 'NONE',  ( 0.000000000000000000, 0.000000000000000000, 0.000000000000000000 ) ) ;
#1592=CARTESIAN_POINT ( 'NONE',  ( 0.3126073911695753660, -2.020725942163847932, -3.499999999999975131 ) ) ;
#1638=AXIS2_PLACEMENT_3D ( 'NONE', #19755, #13874, #17507 ) ;
#1707=CARTESIAN_POINT ( 'NONE',  ( 4.175813232069142344, 2.061359961916322980, 3.570380186727409200 ) ) ;
#1718=CARTESIAN_POINT ( 'NONE',  ( 5.600000000000000533, -2.020725942163764444, 3.499999999999985789 ) ) ;
#1744=EDGE_CURVE ( 'NONE', #14430, #21672, #18257, .T. ) ;
#1749=CARTESIAN_POINT ( 'NONE',  ( 5.100000000000000533, 0.000000000000000000, -3.469446951953614189E-15 ) ) ;
#1750=CARTESIAN_POINT ( 'NONE',  ( 3.972066048304784491, -3.435565134476505911, -1.180968096049849869 ) ) ;
#1752=CARTESIAN_POINT ( 'NONE',  ( -3.092868566891418549E-14, 2.686816014504519678, 2.346298152288352146 ) ) ;
#1777=ORIENTED_EDGE ( 'NONE', *, *, #22734, .T. ) ;
#1813=CARTESIAN_POINT ( 'NONE',  ( 0.000000000000000000, 0.000000000000000000, 3.499999999999975131 ) ) ;
#1852=EDGE_CURVE ( 'NONE', #3527, #7794, #275, .T. ) ;
#1863=CARTESIAN_POINT ( 'NONE',  ( 4.033901012035399525, -2.321269032828001233, -2.979444097106729750 ) ) ;
#1872=CARTESIAN_POINT ( 'NONE',  ( 4.158413352280815545, 2.044871626972852408, -3.541821552872977286 ) ) ;
#1873=CARTESIAN_POINT ( 'NONE',  ( 3.878096787214420083, -2.680238624820968418, 2.357690525401573645 ) ) ;
#1930=CARTESIAN_POINT ( 'NONE',  ( 0.1217565302851083830, -2.351289329882206403, -2.927447417349482883 ) ) ;
#1969=B_SPLINE_CURVE_WITH_KNOTS ( 'NONE', 3,
 ( #22394, #11321, #5930, #4147, #9577, #16954 ),
 .UNSPECIFIED., .F., .F.,
 ( 4, 2, 4 ),
 ( 0.002044882221487500686, 0.003063384235218499785, 0.004081886248949498017 ),
 .UNSPECIFIED. ) ;
#2008=AXIS2_PLACEMENT_3D ( 'NONE', #4771, #3017, #6657 ) ;
#2032=AXIS2_PLACEMENT_3D ( 'NONE', #3124, #22998, #6884 ) ;
#2047=EDGE_CURVE ( 'NONE', #12739, #15071, #304, .T. ) ;
#2048=CARTESIAN_POINT ( 'NONE',  ( 4.158413352280808439, -2.044871626972824430, -3.541821552872959966 ) ) ;
#2086=ORIENTED_EDGE ( 'NONE', *, *, #2342, .F. ) ;
#2094=CARTESIAN_POINT ( 'NONE',  ( 4.175813232069149450, 2.061359961916364725, -3.570380186727398986 ) ) ;
#2107=CARTESIAN_POINT ( 'NONE',  ( 3.958484000407791914, 2.327740518749039644, -2.968235154689956801 ) ) ;
#2127=( BOUNDED_SURFACE ( )  B_SPLINE_SURFACE ( 3, 2, ( 
 ( #13391, #12069, #19148 ),
 ( #4558, #18927, #11733 ),
 ( #19259, #13747, #20929 ),
 ( #4795, #20575, #10202 ),
 ( #17371, #1052, #22452 ),
 ( #6685, #6342, #13857 ) ),
 .UNSPECIFIED., .F., .F., .F. ) 
 B_SPLINE_SURFACE_WITH_KNOTS ( ( 4, 2, 4 ),
 ( 3, 3 ),
 ( 0.01651999345535505592, 0.01858032176739835006, 0.02064065007944164767 ),
 ( 0.000000000000000000, 1.000000000000000000 ),
 .UNSPECIFIED. ) 
 GEOMETRIC_REPRESENTATION_ITEM ( )  RATIONAL_B_SPLINE_SURFACE ( (
 ( 1.000000000000000000, 0.8047781103519399126, 1.000000000000000000),
 ( 1.000000000000000000, 0.8123785825599758592, 1.000000000000000000),
 ( 1.000000000000000000, 0.8190671539794385225, 1.000000000000000000),
 ( 1.000000000000000000, 0.8192352254828778602, 1.000000000000000000),
 ( 1.000000000000000000, 0.8126129677216167302, 1.000000000000000000),
 ( 1.000000000000000000, 0.8047712537969725632, 1.000000000000000000) ) ) 
 REPRESENTATION_ITEM ( '' )  SURFACE ( )  );
#2163=CARTESIAN_POINT ( 'NONE',  ( 3.951447005078452701, -2.357513599190993681, -2.916666666666662078 ) ) ;
#2199=EDGE_CURVE ( 'NONE', #8317, #11002, #5565, .T. ) ;
#2224=ADVANCED_FACE ( 'NONE', ( #4686 ), #5585, .T. ) ;
#2225=CARTESIAN_POINT ( 'NONE',  ( 5.100000000000000533, 1.758911592640616865E-31, 5.200000000000004619 ) ) ;
#2282=CARTESIAN_POINT ( 'NONE',  ( 0.02993401039715375481, 2.688325911136459911, -2.343682934607804746 ) ) ;
#2285=DIRECTION ( 'NONE',  ( 0.000000000000000000, 1.000000000000000000, -6.383782391594650107E-16 ) ) ;
#2309=ADVANCED_FACE ( 'NONE', ( #17493 ), #2127, .F. ) ;
#2316=CARTESIAN_POINT ( 'NONE',  ( 4.158921444904714271, -2.089933220600045605, -3.500000000000009326 ) ) ;
#2325=ORIENTED_EDGE ( 'NONE', *, *, #16245, .T. ) ;
#2342=EDGE_CURVE ( 'NONE', #14430, #1004, #14213, .T. ) ;
#2408=EDGE_LOOP ( 'NONE', ( #9819, #16490, #3078, #11320, #18097 ) ) ;
#2437=CARTESIAN_POINT ( 'NONE',  ( 4.086375874528099139, -2.103253014742889171, -3.500000000000010214 ) ) ;
#2450=AXIS2_PLACEMENT_3D ( 'NONE', #486, #22586, #20713 ) ;
#2457=FACE_OUTER_BOUND ( 'NONE', #1299, .T. ) ;
#2470=EDGE_CURVE ( 'NONE', #13557, #17638, #8665, .T. ) ;
#2478=DIRECTION ( 'NONE',  ( 1.000000000000000000, 1.479114197289397135E-31, -7.395570986446975166E-31 ) ) ;
#2479=CARTESIAN_POINT ( 'NONE',  ( 0.1388410611045837739, 3.710337782247994820, 0.5735064479039461149 ) ) ;
#2508=CARTESIAN_POINT ( 'NONE',  ( 5.600000000000000533, 0.000000000000000000, -3.469446951953614189E-15 ) ) ;
#2512=CARTESIAN_POINT ( 'NONE',  ( 4.180231680468780020, -2.085385483809547136, 3.570466434508575926 ) ) ;
#2528=EDGE_LOOP ( 'NONE', ( #5964, #777, #21753, #424, #12855 ) ) ;
#2535=CARTESIAN_POINT ( 'NONE',  ( 4.175326769692852658, -4.121399112977865542, -6.938946365301216616E-15 ) ) ;
#2549=CARTESIAN_POINT ( 'NONE',  ( 25.60000000000000142, 0.000000000000000000, -6.938893903907228378E-15 ) ) ;
#2577=( GEOMETRIC_REPRESENTATION_CONTEXT ( 3 ) GLOBAL_UNCERTAINTY_ASSIGNED_CONTEXT ( ( #10247 ) ) GLOBAL_UNIT_ASSIGNED_CONTEXT ( ( #7825, #14880, #7366 ) ) REPRESENTATION_CONTEXT ( 'NONE', 'WORKASPACE' ) );
#2602=DIRECTION ( 'NONE',  ( -0.7071067811865530128, -8.067112339249838682E-32, 0.7071067811865421326 ) ) ;
#2634=CARTESIAN_POINT ( 'NONE',  ( 3.974183935050594307, -0.7239581970533454092, 3.565826011443202770 ) ) ;
#2635=EDGE_CURVE ( 'NONE', #11002, #8317, #15741, .T. ) ;
#2654=CARTESIAN_POINT ( 'NONE',  ( 4.158413352280808439, 2.044871626972768919, 3.541821552872997714 ) ) ;
#2702=CARTESIAN_POINT ( 'NONE',  ( 4.093692494532776394, 4.043567292011502445, 6.937578715282024528E-15 ) ) ;
#2719=CONICAL_SURFACE ( 'NONE', #16247, 2.055000000000002380, 0.7853981633974400633 ) ;
#2730=DIRECTION ( 'NONE',  ( -7.395570986446975166E-31, -3.382522293539642681E-32, -1.000000000000000000 ) ) ;
#2735=B_SPLINE_CURVE_WITH_KNOTS ( 'NONE', 3,
 ( #9115, #2163, #16388, #9350, #16616 ),
 .UNSPECIFIED., .F., .F.,
 ( 4, 1, 4 ),
 ( 0.000000000000000000, 0.002020725942163690073, 0.004041451884327380145 ),
 .UNSPECIFIED. ) ;
#2774=DIRECTION ( 'NONE',  ( 5.423418723394450907E-31, 0.5000000000000015543, 0.8660254037844377084 ) ) ;
#2776=CARTESIAN_POINT ( 'NONE',  ( 4.175572532730933872, 2.061029303918013866, 3.569807470274402483 ) ) ;
#2793=VECTOR ( 'NONE', #2602, 999.9999999999998863 ) ;
#2823=EDGE_CURVE ( 'NONE', #19662, #6728, #6418, .T. ) ;
#2825=ORIENTED_EDGE ( 'NONE', *, *, #11116, .T. ) ;
#2838=CARTESIAN_POINT ( 'NONE',  ( 0.02993401039710850628, 3.373851915354574516, 1.156317065392207688 ) ) ;
#2857=CARTESIAN_POINT ( 'NONE',  ( 25.60000000000000142, 0.000000000000000000, -6.938893903907228378E-15 ) ) ;
#2867=EDGE_CURVE ( 'NONE', #15390, #20382, #9716, .T. ) ;
#2911=DIRECTION ( 'NONE',  ( 0.000000000000000000, 3.382522293539643228E-32, 1.000000000000000000 ) ) ;
#2963=DIRECTION ( 'NONE',  ( 0.000000000000000000, 0.000000000000000000, 1.000000000000000000 ) ) ;
#2966=ORIENTED_EDGE ( 'NONE', *, *, #9531, .T. ) ;
#2987=EDGE_CURVE ( 'NONE', #7794, #19662, #2735, .T. ) ;
#3005=LINE ( 'NONE', #11584, #12546 ) ;
#3017=DIRECTION ( 'NONE',  ( -1.000000000000000000, -1.479114197289397135E-31, -5.916456789157588541E-31 ) ) ;
#3077=EDGE_CURVE ( 'NONE', #15429, #20382, #22076, .T. ) ;
#3078=ORIENTED_EDGE ( 'NONE', *, *, #12818, .T. ) ;
#3101=CARTESIAN_POINT ( 'NONE',  ( 3.948095570616719563, 0.6965071952228556462, 3.499999999999969358 ) ) ;
#3124=CARTESIAN_POINT ( 'NONE',  ( 5.600000000000000533, 4.041451884327335264, -1.734723475976807094E-14 ) ) ;
#3191=B_SPLINE_CURVE_WITH_KNOTS ( 'NONE', 3,
 ( #22659, #11590, #15114, #13246, #11934, #19013, #22310, #4410, #18777, #2654, #9958, #4764, #22421, #6197, #2776, #20430 ),
 .UNSPECIFIED., .F., .F.,
 ( 4, 3, 3, 3, 3, 4 ),
 ( 0.000000000000000000, 3.315506744709155554E-05, 6.608280158698813327E-05, 0.0001026520855291346973, 0.0001376952025664800172, 0.0001398064759190610737 ),
 .UNSPECIFIED. ) ;
#3194=CARTESIAN_POINT ( 'NONE',  ( 4.071447262713884463, -2.020725942163709377, 3.500000000000003109 ) ) ;
#3211=ORIENTED_EDGE ( 'NONE', *, *, #15485, .T. ) ;
#3222=EDGE_CURVE ( 'NONE', #21815, #20382, #588, .T. ) ;
#3257=CARTESIAN_POINT ( 'NONE',  ( 0.000000000000000000, 0.000000000000000000, 0.000000000000000000 ) ) ;
#3312=CARTESIAN_POINT ( 'NONE',  ( 4.142654963991865280, 2.035398498734349637, -3.525413613457325734 ) ) ;
#3318=ORIENTED_EDGE ( 'NONE', *, *, #2199, .F. ) ;
#3364=CARTESIAN_POINT ( 'NONE',  ( 0.3126073911696378160, -2.020725942163709377, 3.500000000000003109 ) ) ;
#3396=CARTESIAN_POINT ( 'NONE',  ( 4.050880675075974047, 1.379097446046313902, 3.567934390854443194 ) ) ;
#3435=AXIS2_PLACEMENT_3D ( 'NONE', #2225, #7637, #17884 ) ;
#3467=CARTESIAN_POINT ( 'NONE',  ( 0.000000000000000000, 0.000000000000000000, 3.499999999999975131 ) ) ;
#3471=DIRECTION ( 'NONE',  ( -1.000000000000000000, -1.479114197289397135E-31, -5.916456789157588541E-31 ) ) ;
#3483=CARTESIAN_POINT ( 'NONE',  ( 4.071447262713891568, -2.020725942163709377, -3.499999999999999556 ) ) ;
#3504=CIRCLE ( 'NONE', #1638, 2.500000000000003997 ) ;
#3524=CIRCLE ( 'NONE', #10653, 3.500000000000004441 ) ;
#3527=VERTEX_POINT ( 'NONE', #13636 ) ;
#3533=FACE_OUTER_BOUND ( 'NONE', #11873, .T. ) ;
#3555=ORIENTED_EDGE ( 'NONE', *, *, #21049, .F. ) ;
#3556=CLOSED_SHELL ( 'NONE', ( #776, #2224, #11261, #5049, #11846, #352, #8243, #13392, #22580, #19269, #19759, #9442, #4069, #18165, #19024, #3787, #69, #9250, #19718, #16371, #5190, #12684, #10694, #5867, #641, #17883, #22382, #2309, #18646 ) ) ;
#3584=ORIENTED_EDGE ( 'NONE', *, *, #611, .F. ) ;
#3594=DIRECTION ( 'NONE',  ( 0.000000000000000000, 3.382522293539642681E-32, 1.000000000000000000 ) ) ;
#3614=CARTESIAN_POINT ( 'NONE',  ( 3.972709601346601449, -3.429395227388333023, -1.191688283765310885 ) ) ;
#3635=DIRECTION ( 'NONE',  ( -7.395570986446975166E-31, -3.382522293539642681E-32, -1.000000000000000000 ) ) ;
#3641=CARTESIAN_POINT ( 'NONE',  ( 4.180345304246205984, -4.135116856707421462, 0.02129519942685456982 ) ) ;
#3652=CARTESIAN_POINT ( 'NONE',  ( 4.093692494532771065, 2.021783646005777424, -3.501831996793832502 ) ) ;
#3701=CARTESIAN_POINT ( 'NONE',  ( 4.114405500665258231, -2.025575754679721729, -3.508400121684964290 ) ) ;
#3723=CARTESIAN_POINT ( 'NONE',  ( 3.973110223768726801, 0.6864646529411468912, 3.565797985667434222 ) ) ;
#3744=PRODUCT_DEFINITION_FORMATION_WITH_SPECIFIED_SOURCE ( 'ANY', '', #23234, .NOT_KNOWN. ) ;
#3745=CARTESIAN_POINT ( 'NONE',  ( 4.158921614371315911, -4.076055977742331748, 0.05993604794446181355 ) ) ;
#3755=CARTESIAN_POINT ( 'NONE',  ( 4.086262629614036079, -4.082406995610011080, -0.07093633357111590876 ) ) ;
#3771=DIRECTION ( 'NONE',  ( -7.395570986446975166E-31, -3.382522293539642681E-32, -1.000000000000000000 ) ) ;
#3787=ADVANCED_FACE ( 'NONE', ( #15471 ), #12729, .T. ) ;
#3858=CARTESIAN_POINT ( 'NONE',  ( 4.158806965674322065, -1.986429158307121412, -3.559403772175879332 ) ) ;
#3898=FACE_OUTER_BOUND ( 'NONE', #11810, .T. ) ;
#3932=CARTESIAN_POINT ( 'NONE',  ( 4.175813232069149450, -4.122719923832729449, 0.000000000000000000 ) ) ;
#3968=B_SPLINE_CURVE_WITH_KNOTS ( 'NONE', 3,
 ( #3194, #8593, #22957, #21875, #19883 ),
 .UNSPECIFIED., .F., .F.,
 ( 4, 1, 4 ),
 ( 0.000000000000000000, 0.002020725942163685736, 0.004041451884327371472 ),
 .UNSPECIFIED. ) ;
#3976=CARTESIAN_POINT ( 'NONE',  ( 4.086376042167614742, -4.082715877136890548, 0.07147133206913598713 ) ) ;
#3996=EDGE_CURVE ( 'NONE', #14430, #3527, #20144, .T. ) ;
#4004=CARTESIAN_POINT ( 'NONE',  ( 4.082498951862918446, 4.041451884327377009, -2.081668171172168513E-14 ) ) ;
#4025=EDGE_CURVE ( 'NONE', #9067, #5868, #19854, .T. ) ;
#4056=ORIENTED_EDGE ( 'NONE', *, *, #19456, .F. ) ;
#4069=ADVANCED_FACE ( 'NONE', ( #20407 ), #21351, .T. ) ;
#4072=CARTESIAN_POINT ( 'NONE',  ( 25.15499999999999403, 0.000000000000000000, -6.938893903907228378E-15 ) ) ;
#4081=EDGE_CURVE ( 'NONE', #7132, #10391, #8325, .T. ) ;
#4088=AXIS2_PLACEMENT_3D ( 'NONE', #17240, #18788, #921 ) ;
#4096=FACE_OUTER_BOUND ( 'NONE', #13381, .T. ) ;
#4147=CARTESIAN_POINT ( 'NONE',  ( 0.1388410611046231868, -3.710337782248059657, -0.5735064479039724272 ) ) ;
#4150=B_SPLINE_CURVE_WITH_KNOTS ( 'NONE', 3,
 ( #8107, #15504, #8337, #8461 ),
 .UNSPECIFIED., .F., .F.,
 ( 4, 4 ),
 ( 0.002080789711329242460, 0.004173039763574508225 ),
 .UNSPECIFIED. ) ;
#4152=CARTESIAN_POINT ( 'NONE',  ( 4.093692494532773729, -2.021783646005778312, -3.501831996793871582 ) ) ;
#4174=CARTESIAN_POINT ( 'NONE',  ( 4.104070371397483541, -4.047367226856738220, 0.000000000000000000 ) ) ;
#4240=DIRECTION ( 'NONE',  ( 7.395570986446975166E-31, 3.382522293539642681E-32, 1.000000000000000000 ) ) ;
#4269=DIRECTION ( 'NONE',  ( -1.479114197289397792E-31, 1.000000000000000000, 1.224646799147352961E-16 ) ) ;
#4273=CIRCLE ( 'NONE', #9542, 3.500000000000004441 ) ;
#4279=( LENGTH_UNIT ( ) NAMED_UNIT ( * ) SI_UNIT ( .MILLI., .METRE. ) );
#4304=CARTESIAN_POINT ( 'NONE',  ( 3.880198502136892547, 0.7307680362926917139, -3.500000000000009770 ) ) ;
#4315=DIRECTION ( 'NONE',  ( 1.000000000000000000, 1.479114197289397135E-31, 5.916456789157588541E-31 ) ) ;
#4354=TOROIDAL_SURFACE ( 'NONE', #23166, 5.200000000000001066, 0.4999999999999978351 ) ;
#4403=CARTESIAN_POINT ( 'NONE',  ( 4.124214193018072905, -2.028338413290942110, 3.513185186763558843 ) ) ;
#4410=CARTESIAN_POINT ( 'NONE',  ( 4.142654963991848405, 2.035398498734347417, 3.525413613457328843 ) ) ;
#4439=SHAPE_REPRESENTATION ( 'hex flange bolt small_iso_ISO 4162 - M5 x 20 x 20-N', ( #22115 ), #2577 ) ;
#4477=AXIS2_PLACEMENT_3D ( 'NONE', #4072, #670, #1140 ) ;
#4555=CARTESIAN_POINT ( 'NONE',  ( 0.000000000000000000, 0.000000000000000000, 0.000000000000000000 ) ) ;
#4558=CARTESIAN_POINT ( 'NONE',  ( 3.961551342854056745, 2.319461885623242292, 2.982574167880871485 ) ) ;
#4560=CARTESIAN_POINT ( 'NONE',  ( 0.000000000000000000, 0.000000000000000000, 0.000000000000000000 ) ) ;
#4630=PRODUCT_DEFINITION_CONTEXT ( 'detailed design', #10732, 'design' ) ;
#4640=MECHANICAL_DESIGN_GEOMETRIC_PRESENTATION_REPRESENTATION('',(#10654),#23062);
#4652=TOROIDAL_SURFACE ( 'NONE', #2008, 5.200000000000001066, 0.4999999999999978351 ) ;
#4669=ORIENTED_EDGE ( 'NONE', *, *, #18556, .T. ) ;
#4684=CARTESIAN_POINT ( 'NONE',  ( 2.107079159589796892E-14, -2.859595677584363393, 2.047034997319605143 ) ) ;
#4686=FACE_OUTER_BOUND ( 'NONE', #18531, .T. ) ;
#4729=ORIENTED_EDGE ( 'NONE', *, *, #6094, .T. ) ;
#4764=CARTESIAN_POINT ( 'NONE',  ( 4.170895651974849905, 2.054890354522574292, 3.559174498016395294 ) ) ;
#4771=CARTESIAN_POINT ( 'NONE',  ( 5.100000000000000533, 0.000000000000000000, -3.469446951953614189E-15 ) ) ;
#4778=DIRECTION ( 'NONE',  ( 0.000000000000000000, -3.382522293539642681E-32, -1.000000000000000000 ) ) ;
#4783=VERTEX_POINT ( 'NONE', #5737 ) ;
#4795=CARTESIAN_POINT ( 'NONE',  ( 3.878096787214385444, 3.381939201670001616, 1.142309474598473873 ) ) ;
#4800=DIRECTION ( 'NONE',  ( -7.395570986446975166E-31, -3.382522293539642681E-32, -1.000000000000000000 ) ) ;
#4854=CARTESIAN_POINT ( 'NONE',  ( 4.030875481282551576, 1.403567514398184723, 3.499999999999968026 ) ) ;
#4943=CARTESIAN_POINT ( 'NONE',  ( 0.000000000000000000, 0.000000000000000000, 0.000000000000000000 ) ) ;
#4999=DIRECTION ( 'NONE',  ( -1.000000000000000000, -1.479114197289397135E-31, -5.916456789157588541E-31 ) ) ;
#5049=ADVANCED_FACE ( 'NONE', ( #17701 ), #13831, .T. ) ;
#5062=CARTESIAN_POINT ( 'NONE',  ( 4.071447262713884463, 2.020725942163639655, -3.499999999999996003 ) ) ;
#5067=CARTESIAN_POINT ( 'NONE',  ( 4.052424581287842997, -2.393186648133572625, 2.990837702970500445 ) ) ;
#5124=CARTESIAN_POINT ( 'NONE',  ( 4.071447262713884463, 2.020725942163639655, -3.499999999999996003 ) ) ;
#5190=ADVANCED_FACE ( 'NONE', ( #9235 ), #294, .F. ) ;
#5201=ORIENTED_EDGE ( 'NONE', *, *, #9120, .T. ) ;
#5236=AXIS2_PLACEMENT_3D ( 'NONE', #10182, #13834, #16992 ) ;
#5259=LINE ( 'NONE', #1718, #17971 ) ;
#5264=ORIENTED_EDGE ( 'NONE', *, *, #217, .T. ) ;
#5281=CARTESIAN_POINT ( 'NONE',  ( 4.158807179406254662, 2.089320655794529191, -3.500000000000009326 ) ) ;
#5298=CARTESIAN_POINT ( 'NONE',  ( 4.175813232069149450, 2.061359961916364725, -3.570380186727398986 ) ) ;
#5306=DIRECTION ( 'NONE',  ( 1.000000000000000000, 0.000000000000000000, 0.000000000000000000 ) ) ;
#5340=ORIENTED_EDGE ( 'NONE', *, *, #10018, .T. ) ;
#5361=DIRECTION ( 'NONE',  ( -1.000000000000000000, -1.479114197289397135E-31, -5.916456789157588541E-31 ) ) ;
#5371=EDGE_CURVE ( 'NONE', #19811, #16509, #20365, .T. ) ;
#5390=CARTESIAN_POINT ( 'NONE',  ( 4.175813232069149450, -4.122719923832729449, 0.000000000000000000 ) ) ;
#5420=CARTESIAN_POINT ( 'NONE',  ( 25.60000000000000142, 6.951083313223974888E-32, 2.054999999999995719 ) ) ;
#5429=CARTESIAN_POINT ( 'NONE',  ( 4.124214193018077346, 2.028338413290940778, -3.513185186763563728 ) ) ;
#5430=CARTESIAN_POINT ( 'NONE',  ( 4.180231891692627322, -4.134807952925598329, -0.02076457676761531146 ) ) ;
#5476=CARTESIAN_POINT ( 'NONE',  ( 4.142654963991851957, -2.035398498734401596, -3.525413613457302198 ) ) ;
#5484=CARTESIAN_POINT ( 'NONE',  ( 3.973110223767149840, -2.262799480050941678E-11, -3.565797985667468417 ) ) ;
#5529=DIRECTION ( 'NONE',  ( -1.000000000000000000, -1.479114197289397135E-31, -5.916456789157588541E-31 ) ) ;
#5565=CIRCLE ( 'NONE', #15302, 2.500000000000003997 ) ;
#5577=ORIENTED_EDGE ( 'NONE', *, *, #11369, .F. ) ;
#5585=CONICAL_SURFACE ( 'NONE', #11576, 5.371010071662839280, 1.221730476396037490 ) ;
#5621=CARTESIAN_POINT ( 'NONE',  ( 3.973110223767125859, 2.263145622885971846E-11, 3.565797985667392922 ) ) ;
#5737=CARTESIAN_POINT ( 'NONE',  ( 0.3126073911696378160, -2.020725942163709377, 3.500000000000003109 ) ) ;
#5769=CARTESIAN_POINT ( 'NONE',  ( 4.052424581287912275, 2.393186648133639238, -2.990837702970695400 ) ) ;
#5781=SHAPE_DEFINITION_REPRESENTATION ( #13619, #4439 ) ;
#5803=CARTESIAN_POINT ( 'NONE',  ( 0.000000000000000000, 0.000000000000000000, 0.000000000000000000 ) ) ;
#5824=ORIENTED_EDGE ( 'NONE', *, *, #8630, .T. ) ;
#5867=ADVANCED_FACE ( 'NONE', ( #7191 ), #21401, .F. ) ;
#5868=VERTEX_POINT ( 'NONE', #16216 ) ;
#5904=DIRECTION ( 'NONE',  ( 1.000000000000000000, 1.479114197289397135E-31, 5.916456789157588541E-31 ) ) ;
#5923=ORIENTED_EDGE ( 'NONE', *, *, #6250, .T. ) ;
#5930=CARTESIAN_POINT ( 'NONE',  ( 0.02993401039714900166, -3.373851915354638020, -1.156317065392238774 ) ) ;
#5934=DIRECTION ( 'NONE',  ( 0.000000000000000000, 3.382522293539642681E-32, 1.000000000000000000 ) ) ;
#5937=CARTESIAN_POINT ( 'NONE',  ( 4.124214193018073793, -2.028338413290998510, -3.513185186763549961 ) ) ;
#5964=ORIENTED_EDGE ( 'NONE', *, *, #22734, .F. ) ;
#5974=AXIS2_PLACEMENT_3D ( 'NONE', #2549, #16425, #16766 ) ;
#6040=AXIS2_PLACEMENT_3D ( 'NONE', #16012, #10496, #22977 ) ;
#6052=CARTESIAN_POINT ( 'NONE',  ( 4.086262418390188778, -2.102635014057370189, 3.499999999999970690 ) ) ;
#6073=CARTESIAN_POINT ( 'NONE',  ( 4.158413352280808439, -4.089743253945677282, -2.775557561562891351E-14 ) ) ;
#6094=EDGE_CURVE ( 'NONE', #17638, #927, #4150, .T. ) ;
#6113=DIRECTION ( 'NONE',  ( 0.3420201433256618850, 1.880337258636373401E-32, -0.9396926207859108704 ) ) ;
#6114=CARTESIAN_POINT ( 'NONE',  ( 4.033901012036838374, 3.740908793663468845, -0.5205559028929584997 ) ) ;
#6131=CARTESIAN_POINT ( 'NONE',  ( 4.175075985190096262, 4.120741555260251765, -2.775557561562891351E-14 ) ) ;
#6167=CARTESIAN_POINT ( 'NONE',  ( 3.806834918298588555, 3.031088913245420180, 1.749999999999915623 ) ) ;
#6195=CARTESIAN_POINT ( 'NONE',  ( 4.071447262713891568, -4.041451884327432076, 1.040834085586084257E-14 ) ) ;
#6197=CARTESIAN_POINT ( 'NONE',  ( 4.175326769692855322, 2.060699556488938544, 3.569236330973458049 ) ) ;
#6211=ORIENTED_EDGE ( 'NONE', *, *, #7675, .F. ) ;
#6228=CARTESIAN_POINT ( 'NONE',  ( 3.973110223767125859, 2.263145622885971846E-11, 3.565797985667392922 ) ) ;
#6250=EDGE_CURVE ( 'NONE', #17638, #15390, #23050, .T. ) ;
#6295=ORIENTED_EDGE ( 'NONE', *, *, #217, .F. ) ;
#6306=CARTESIAN_POINT ( 'NONE',  ( 4.114405500665259119, -2.025575754679708407, 3.508400121684940753 ) ) ;
#6326=DIRECTION ( 'NONE',  ( 1.000000000000000000, 1.479114197289397135E-31, 5.916456789157588541E-31 ) ) ;
#6342=CARTESIAN_POINT ( 'NONE',  ( 4.158921614371280384, 4.076055977742235825, -0.05993604794454210349 ) ) ;
#6373=CARTESIAN_POINT ( 'NONE',  ( 0.000000000000000000, 3.031088913245508110, -1.750000000000029310 ) ) ;
#6381=AXIS2_PLACEMENT_3D ( 'NONE', #14234, #5529, #19984 ) ;
#6418=B_SPLINE_CURVE_WITH_KNOTS ( 'NONE', 3,
 ( #10295, #16158, #14298, #12169, #1475 ),
 .UNSPECIFIED., .F., .F.,
 ( 4, 1, 4 ),
 ( 0.000000000000000000, 0.002020725942163693108, 0.004041451884327386217 ),
 .UNSPECIFIED. ) ;
#6422=CARTESIAN_POINT ( 'NONE',  ( 4.170895651974856122, -2.054890354522733720, 3.559174498016319799 ) ) ;
#6445=VERTEX_POINT ( 'NONE', #12788 ) ;
#6453=CARTESIAN_POINT ( 'NONE',  ( 4.630153689607049650, 0.000000000000000000, -3.469446951953614189E-15 ) ) ;
#6501=CARTESIAN_POINT ( 'NONE',  ( 3.973514160553446306, 2.741076955031306550, 2.383932505289861670 ) ) ;
#6504=CARTESIAN_POINT ( 'NONE',  ( 3.951447005078449148, 3.704664227300095813, 0.5833333333333124981 ) ) ;
#6518=DIRECTION ( 'NONE',  ( 1.000000000000000000, 1.479114197289397135E-31, 5.916456789157588541E-31 ) ) ;
#6657=DIRECTION ( 'NONE',  ( -5.916456789157588541E-31, 3.382522293539642681E-32, 1.000000000000000000 ) ) ;
#6667=VERTEX_POINT ( 'NONE', #390 ) ;
#6685=CARTESIAN_POINT ( 'NONE',  ( 4.086376042167580103, 4.082715877136795513, -0.07147133206921667259 ) ) ;
#6728=VERTEX_POINT ( 'NONE', #620 ) ;
#6804=CARTESIAN_POINT ( 'NONE',  ( 4.630153689607049650, 6.577590292450094690E-16, 5.371010071662835728 ) ) ;
#6811=CIRCLE ( 'NONE', #3435, 0.4999999999999978351 ) ;
#6853=( BOUNDED_SURFACE ( )  B_SPLINE_SURFACE ( 3, 2, ( 
 ( #23173, #5281, #22090 ),
 ( #16537, #13032, #7508 ),
 ( #4304, #20324, #14671 ),
 ( #13261, #570, #21978 ),
 ( #20096, #443, #9496 ),
 ( #2437, #2316, #7620 ) ),
 .UNSPECIFIED., .F., .F., .T. ) 
 B_SPLINE_SURFACE_WITH_KNOTS ( ( 4, 2, 4 ),
 ( 3, 3 ),
 ( 0.01652267773200354062, 0.01858309280828997906, 0.02064350788457642097 ),
 ( 0.000000000000000000, 1.000000000000000000 ),
 .UNSPECIFIED. ) 
 GEOMETRIC_REPRESENTATION_ITEM ( )  RATIONAL_B_SPLINE_SURFACE ( (
 ( 1.000000000000000000, 0.8047780975688292315, 1.000000000000000000),
 ( 1.000000000000000000, 0.8123789546323675337, 1.000000000000000000),
 ( 1.000000000000000000, 0.8190677982989954531, 1.000000000000000000),
 ( 1.000000000000000000, 0.8192346069550978660, 1.000000000000000000),
 ( 1.000000000000000000, 0.8126126759769800589, 1.000000000000000000),
 ( 1.000000000000000000, 0.8047712639312011307, 1.000000000000000000) ) ) 
 REPRESENTATION_ITEM ( '' )  SURFACE ( )  );
#6884=DIRECTION ( 'NONE',  ( -8.381647117973248681E-31, 0.5000000000000012212, -0.8660254037844379305 ) ) ;
#6928=CARTESIAN_POINT ( 'NONE',  ( 4.630153689607049650, -1.816756130622550821E-31, -5.371010071662842833 ) ) ;
#6963=CARTESIAN_POINT ( 'NONE',  ( 4.175572532730932984, 2.061029303918059608, -3.569807470274386052 ) ) ;
#6971=CIRCLE ( 'NONE', #11462, 3.500000000000004441 ) ;
#7032=ORIENTED_EDGE ( 'NONE', *, *, #14672, .F. ) ;
#7132=VERTEX_POINT ( 'NONE', #22116 ) ;
#7174=ORIENTED_EDGE ( 'NONE', *, *, #22283, .T. ) ;
#7181=DIRECTION ( 'NONE',  ( 7.395570986446975166E-31, 3.382522293539642681E-32, 1.000000000000000000 ) ) ;
#7185=CARTESIAN_POINT ( 'NONE',  ( -1.848892746611746769E-30, 3.061616997868387085E-16, -2.500000000000003997 ) ) ;
#7191=FACE_OUTER_BOUND ( 'NONE', #11924, .T. ) ;
#7196=ORIENTED_EDGE ( 'NONE', *, *, #19460, .T. ) ;
#7251=CARTESIAN_POINT ( 'NONE',  ( 4.175813232069149450, 4.122719923832687705, 1.040834085586084257E-14 ) ) ;
#7268=CARTESIAN_POINT ( 'NONE',  ( 4.050823680195226650, -2.400527758044912474, -2.978030508226150452 ) ) ;
#7279=COLOUR_RGB ( '', 0.66274510, 0.83137255, 0.94901961) ;
#7288=CONICAL_SURFACE ( 'NONE', #10259, 3.500000000000004441, 1.047197551196600296 ) ;
#7320=EDGE_LOOP ( 'NONE', ( #9337, #11847, #14534 ) ) ;
#7326=CARTESIAN_POINT ( 'NONE',  ( 5.600000000000000533, 1.758911592640616865E-31, 5.200000000000004619 ) ) ;
#7355=CARTESIAN_POINT ( 'NONE',  ( 4.170895651974845464, -2.054890354522496132, -3.559174498016470345 ) ) ;
#7366=( NAMED_UNIT ( * ) SI_UNIT ( $, .STERADIAN. ) SOLID_ANGLE_UNIT ( ) );
#7392=CARTESIAN_POINT ( 'NONE',  ( 4.175813232069149450, -4.122719923832729449, 0.000000000000000000 ) ) ;
#7433=( BOUNDED_SURFACE ( )  B_SPLINE_SURFACE ( 3, 2, ( 
 ( #6052, #16617, #2512 ),
 ( #13111, #11449, #18516 ),
 ( #13221, #20405, #2634 ),
 ( #9810, #3101, #8284 ),
 ( #13693, #4854, #15666 ),
 ( #10381, #20985, #19097 ) ),
 .UNSPECIFIED., .F., .F., .F. ) 
 B_SPLINE_SURFACE_WITH_KNOTS ( ( 4, 2, 4 ),
 ( 3, 3 ),
 ( 0.01651732063679903564, 0.01857756227444015695, 0.02063780391208127479 ),
 ( 0.000000000000000000, 1.000000000000000000 ),
 .UNSPECIFIED. ) 
 GEOMETRIC_REPRESENTATION_ITEM ( )  RATIONAL_B_SPLINE_SURFACE ( (
 ( 1.000000000000000000, 0.8047781231227471022, 1.000000000000000000),
 ( 1.000000000000000000, 0.8123782108667384483, 1.000000000000000000),
 ( 1.000000000000000000, 0.8190665102130285646, 1.000000000000000000),
 ( 1.000000000000000000, 0.8192358432847179905, 1.000000000000000000),
 ( 1.000000000000000000, 0.8126132624432910179, 1.000000000000000000),
 ( 1.000000000000000000, 0.8047712436238864120, 1.000000000000000000) ) ) 
 REPRESENTATION_ITEM ( '' )  SURFACE ( )  );
#7441=CARTESIAN_POINT ( 'NONE',  ( 4.630153689607049650, 6.577590292450094690E-16, 5.371010071662835728 ) ) ;
#7474=CARTESIAN_POINT ( 'NONE',  ( 5.600000000000000533, 2.020725942163612121, 3.499999999999957812 ) ) ;
#7500=CIRCLE ( 'NONE', #6381, 2.500000000000003997 ) ;
#7501=EDGE_CURVE ( 'NONE', #1178, #13386, #17994, .T. ) ;
#7508=CARTESIAN_POINT ( 'NONE',  ( 4.055487192203222513, 1.409979666030580114, -3.568038521265891827 ) ) ;
#7518=CARTESIAN_POINT ( 'NONE',  ( 3.974175853610027342, -2.726149789692876801, -2.409821656223177566 ) ) ;
#7547=CARTESIAN_POINT ( 'NONE',  ( 4.170895651974840135, 4.109780709045198321, 2.116862463031252292E-13 ) ) ;
#7587=DIRECTION ( 'NONE',  ( 1.000000000000000000, 1.479114197289397135E-31, 5.916456789157588541E-31 ) ) ;
#7589=ORIENTED_EDGE ( 'NONE', *, *, #18556, .F. ) ;
#7594=ORIENTED_EDGE ( 'NONE', *, *, #14038, .T. ) ;
#7602=CARTESIAN_POINT ( 'NONE',  ( 4.142654963991861727, -4.070796997468701051, 2.081660976370999833E-14 ) ) ;
#7620=CARTESIAN_POINT ( 'NONE',  ( 4.180345136606689493, -2.085999704580133507, -3.570468642550126415 ) ) ;
#7627=EDGE_CURVE ( 'NONE', #1330, #21815, #17899, .T. ) ;
#7637=DIRECTION ( 'NONE',  ( 1.479114197289397135E-31, -1.000000000000000000, 3.382522293539642681E-32 ) ) ;
#7662=CONICAL_SURFACE ( 'NONE', #20835, 3.500000000000004441, 1.047197551196600296 ) ;
#7663=CARTESIAN_POINT ( 'NONE',  ( 4.124214193018068464, 4.056676826581881556, 3.377256047658116025E-15 ) ) ;
#7670=DIRECTION ( 'NONE',  ( -7.395570986446975166E-31, -3.382522293539642681E-32, -1.000000000000000000 ) ) ;
#7675=EDGE_CURVE ( 'NONE', #6667, #5868, #19889, .T. ) ;
#7683=ORIENTED_EDGE ( 'NONE', *, *, #12856, .F. ) ;
#7720=PLANE ( 'NONE',  #20373 ) ;
#7729=FACE_OUTER_BOUND ( 'NONE', #7320, .T. ) ;
#7746=PLANE ( 'NONE',  #12154 ) ;
#7781=AXIS2_PLACEMENT_3D ( 'NONE', #15991, #19652, #12348 ) ;
#7794=VERTEX_POINT ( 'NONE', #3483 ) ;
#7815=CARTESIAN_POINT ( 'NONE',  ( 0.3126073911696447549, -4.041451884327432076, 3.469446951953614189E-15 ) ) ;
#7819=CARTESIAN_POINT ( 'NONE',  ( 0.3126073911696447549, 2.020725942163625888, -3.499999999999996003 ) ) ;
#7825=( LENGTH_UNIT ( ) NAMED_UNIT ( * ) SI_UNIT ( .MILLI., .METRE. ) );
#7833=CARTESIAN_POINT ( 'NONE',  ( 4.158413352280815545, -2.044871626972879941, 3.541821552872997714 ) ) ;
#7837=CARTESIAN_POINT ( 'NONE',  ( 4.175572532730936537, -4.122058607836112110, 2.481766680540189602E-17 ) ) ;
#7872=CARTESIAN_POINT ( 'NONE',  ( 4.630153689607049650, -1.816756130622550821E-31, -5.371010071662842833 ) ) ;
#7900=LINE ( 'NONE', #14954, #2793 ) ;
#7951=CARTESIAN_POINT ( 'NONE',  ( 4.124214193018073793, -4.056676826581885997, 2.081674651455615798E-14 ) ) ;
#7977=DIRECTION ( 'NONE',  ( -7.395570986446975166E-31, -3.382522293539642681E-32, -1.000000000000000000 ) ) ;
#8048=AXIS2_PLACEMENT_3D ( 'NONE', #14948, #2478, #9433 ) ;
#8062=CARTESIAN_POINT ( 'NONE',  ( 4.175326769692857098, -2.060699556488887474, 3.569236330973490023 ) ) ;
#8088=DIRECTION ( 'NONE',  ( -1.000000000000000000, -1.479114197289397135E-31, -5.916456789157588541E-31 ) ) ;
#8107=CARTESIAN_POINT ( 'NONE',  ( 3.973110223767125859, 2.263145622885971846E-11, 3.565797985667392922 ) ) ;
#8131=CARTESIAN_POINT ( 'NONE',  ( -3.066033393607966922E-14, 3.202582148906679471, 1.452965002680416617 ) ) ;
#8152=SURFACE_STYLE_FILL_AREA ( #17074 ) ;
#8198=B_SPLINE_CURVE_WITH_KNOTS ( 'NONE', 3,
 ( #2094, #14681, #12805, #21867, #18104, #16092 ),
 .UNSPECIFIED., .F., .F.,
 ( 4, 2, 4 ),
 ( 0.000000000000000000, 0.002086519881787260184, 0.004173039763574520368 ),
 .UNSPECIFIED. ) ;
#8239=ORIENTED_EDGE ( 'NONE', *, *, #19460, .F. ) ;
#8243=ADVANCED_FACE ( 'NONE', ( #18915 ), #2719, .T. ) ;
#8246=CARTESIAN_POINT ( 'NONE',  ( 4.071447262713891568, 4.041451884327377009, -2.081668171172168513E-14 ) ) ;
#8257=CARTESIAN_POINT ( 'NONE',  ( 0.1217565302851317949, -3.710888496608955922, 0.5725525826504807014 ) ) ;
#8284=CARTESIAN_POINT ( 'NONE',  ( 3.972058292797660872, 0.6948821373597369178, 3.565770528409109463 ) ) ;
#8285=CARTESIAN_POINT ( 'NONE',  ( 0.000000000000000000, 0.000000000000000000, 0.000000000000000000 ) ) ;
#8295=ORIENTED_EDGE ( 'NONE', *, *, #12427, .F. ) ;
#8299=CARTESIAN_POINT ( 'NONE',  ( 4.132952817037863547, -2.031684012687259955, 3.518979934899753470 ) ) ;
#8311=FACE_OUTER_BOUND ( 'NONE', #13132, .T. ) ;
#8317=VERTEX_POINT ( 'NONE', #23029 ) ;
#8325=B_SPLINE_CURVE_WITH_KNOTS ( 'NONE', 3,
 ( #7819, #14755, #16742, #22170, #20294, #18407 ),
 .UNSPECIFIED., .F., .F.,
 ( 4, 2, 4 ),
 ( 0.01103795673506161555, 0.01206113197427185514, 0.01308430721348209473 ),
 .UNSPECIFIED. ) ;
#8337=CARTESIAN_POINT ( 'NONE',  ( 4.050480423730733470, -1.376911654797405404, 3.567926555162027391 ) ) ;
#8343=ORIENTED_EDGE ( 'NONE', *, *, #4081, .T. ) ;
#8345=ORIENTED_EDGE ( 'NONE', *, *, #16005, .F. ) ;
#8377=EDGE_LOOP ( 'NONE', ( #6295, #11843, #1777, #8345, #11289 ) ) ;
#8415=ORIENTED_EDGE ( 'NONE', *, *, #1485, .T. ) ;
#8439=CARTESIAN_POINT ( 'NONE',  ( 4.175813232069149450, -2.061359961916378492, -3.570380186727402538 ) ) ;
#8454=DIRECTION ( 'NONE',  ( 1.000000000000000000, 1.479114197289397135E-31, 5.916456789157588541E-31 ) ) ;
#8461=CARTESIAN_POINT ( 'NONE',  ( 4.175813232069142344, -2.061359961916364725, 3.570380186727402538 ) ) ;
#8471=VECTOR ( 'NONE', #15976, 1000.000000000000000 ) ;
#8593=CARTESIAN_POINT ( 'NONE',  ( 3.951447005078446484, -1.347150628109143877, 3.500000000000002220 ) ) ;
#8630=EDGE_CURVE ( 'NONE', #21672, #13557, #14763, .T. ) ;
#8653=CARTESIAN_POINT ( 'NONE',  ( 5.600000000000000533, 2.020725942163695166, -3.500000000000034195 ) ) ;
#8665=B_SPLINE_CURVE_WITH_KNOTS ( 'NONE', 3,
 ( #14088, #3396, #3723, #5621 ),
 .UNSPECIFIED., .F., .F.,
 ( 4, 4 ),
 ( 0.000000000000000000, 0.002080789711329242460 ),
 .UNSPECIFIED. ) ;
#8669=ORIENTED_EDGE ( 'NONE', *, *, #2635, .T. ) ;
#8678=B_SPLINE_CURVE_WITH_KNOTS ( 'NONE', 3,
 ( #17645, #6963, #12704, #16100, #19409, #12586, #1872, #21546, #3312, #10477, #5429, #19772, #16215, #3652, #10819, #130 ),
 .UNSPECIFIED., .F., .F.,
 ( 4, 3, 3, 3, 3, 4 ),
 ( -2.111273352579345034E-06, 4.235164736271501695E-22, 3.519286887791630951E-05, 7.191842652066397345E-05, 0.0001049868727093587593, 0.0001382836236822092074 ),
 .UNSPECIFIED. ) ;
#8692=VECTOR ( 'NONE', #21258, 1000.000000000000000 ) ;
#8700=DIRECTION ( 'NONE',  ( -1.000000000000000000, -1.479114197289397135E-31, -5.916456789157588541E-31 ) ) ;
#8712=CARTESIAN_POINT ( 'NONE',  ( 4.158921614371306141, -1.986121848748789498, 3.559936047944491477 ) ) ;
#8767=CARTESIAN_POINT ( 'NONE',  ( 4.630153689607049650, 0.000000000000000000, -3.469446951953614189E-15 ) ) ;
#8824=LINE ( 'NONE', #12451, #8471 ) ;
#8926=CARTESIAN_POINT ( 'NONE',  ( 4.050536630291683871, -2.401306687817038821, 2.976670123173771554 ) ) ;
#8976=FACE_OUTER_BOUND ( 'NONE', #10002, .T. ) ;
#9019=ORIENTED_EDGE ( 'NONE', *, *, #22283, .F. ) ;
#9026=CARTESIAN_POINT ( 'NONE',  ( 25.60000000000000142, 2.789133085058096608E-16, -2.055000000000006821 ) ) ;
#9059=CARTESIAN_POINT ( 'NONE',  ( 3.972066048304704555, -2.740530939476112149, 2.384802634787816622 ) ) ;
#9067=VERTEX_POINT ( 'NONE', #11986 ) ;
#9115=CARTESIAN_POINT ( 'NONE',  ( 4.071447262713891568, -2.020725942163709377, -3.499999999999999556 ) ) ;
#9119=CARTESIAN_POINT ( 'NONE',  ( 1.044713074591974287E-14, -2.686816014504604944, -2.346298152288348593 ) ) ;
#9120=EDGE_CURVE ( 'NONE', #10391, #19811, #3524, .T. ) ;
#9132=AXIS2_PLACEMENT_3D ( 'NONE', #17583, #3471, #10640 ) ;
#9135=ORIENTED_EDGE ( 'NONE', *, *, #14707, .F. ) ;
#9159=FACE_OUTER_BOUND ( 'NONE', #9940, .T. ) ;
#9166=AXIS2_PLACEMENT_3D ( 'NONE', #14337, #12573, #19757 ) ;
#9171=CARTESIAN_POINT ( 'NONE',  ( 25.60000000000000142, 0.000000000000000000, -6.938893903907228378E-15 ) ) ;
#9192=B_SPLINE_CURVE_WITH_KNOTS ( 'NONE', 3,
 ( #20504, #8257, #16936, #13197 ),
 .UNSPECIFIED., .F., .F.,
 ( 4, 4 ),
 ( 2.380739282289325661E-07, 0.002044882221487581784 ),
 .UNSPECIFIED. ) ;
#9216=EDGE_LOOP ( 'NONE', ( #13444, #10197, #19422 ) ) ;
#9225=DIRECTION ( 'NONE',  ( -1.000000000000000000, -1.479114197289397135E-31, -5.916456789157588541E-31 ) ) ;
#9232=CARTESIAN_POINT ( 'NONE',  ( 4.132952817037863547, -2.031684012687315466, -3.518979934899742812 ) ) ;
#9235=FACE_OUTER_BOUND ( 'NONE', #2528, .T. ) ;
#9241=FILL_AREA_STYLE_COLOUR ( '', #16856 ) ;
#9250=ADVANCED_FACE ( 'NONE', ( #12090 ), #21531, .F. ) ;
#9280=CARTESIAN_POINT ( 'NONE',  ( 3.878096787214585284, -3.381939201670153938, -1.142309474598458774 ) ) ;
#9337=ORIENTED_EDGE ( 'NONE', *, *, #23179, .T. ) ;
#9348=PRODUCT_DEFINITION ( 'UNKNOWN', '', #3744, #4630 ) ;
#9349=CARTESIAN_POINT ( 'NONE',  ( 0.2174200650117729394, 2.185595227304866661, -3.214438021527967759 ) ) ;
#9350=CARTESIAN_POINT ( 'NONE',  ( 3.951447005078455366, -3.704664227300149548, -0.5833333333333268200 ) ) ;
#9366=ORIENTED_EDGE ( 'NONE', *, *, #11370, .T. ) ;
#9402=CARTESIAN_POINT ( 'NONE',  ( 4.055492966679538291, -2.385006769472565402, -3.005124364834383943 ) ) ;
#9433=DIRECTION ( 'NONE',  ( -7.395570986446975166E-31, -3.382522293539642681E-32, -1.000000000000000000 ) ) ;
#9442=ADVANCED_FACE ( 'NONE', ( #22336 ), #20004, .T. ) ;
#9496=CARTESIAN_POINT ( 'NONE',  ( 4.052416734886668870, -1.393505408945144408, -3.567979131523768555 ) ) ;
#9517=ORIENTED_EDGE ( 'NONE', *, *, #318, .F. ) ;
#9531=EDGE_CURVE ( 'NONE', #1178, #11002, #20923, .T. ) ;
#9542=AXIS2_PLACEMENT_3D ( 'NONE', #3257, #10989, #4240 ) ;
#9577=CARTESIAN_POINT ( 'NONE',  ( 0.2174200650117701361, -3.876582599186239264, -0.2855619784720585530 ) ) ;
#9578=CARTESIAN_POINT ( 'NONE',  ( 0.000000000000000000, 0.000000000000000000, -3.499999999999996003 ) ) ;
#9587=DIRECTION ( 'NONE',  ( -7.395570986446975166E-31, -3.382522293539642681E-32, -1.000000000000000000 ) ) ;
#9590=PRESENTATION_STYLE_ASSIGNMENT (( #12882 ) ) ;
#9640=B_SPLINE_CURVE_WITH_KNOTS ( 'NONE', 3,
 ( #11420, #8131, #2838, #2479, #18958, #10014 ),
 .UNSPECIFIED., .F., .F.,
 ( 4, 2, 4 ),
 ( 0.002044882221487566605, 0.003063384235218515397, 0.004081886248949463322 ),
 .UNSPECIFIED. ) ;
#9662=AXIS2_PLACEMENT_3D ( 'NONE', #1381, #6326, #4778 ) ;
#9684=CARTESIAN_POINT ( 'NONE',  ( 0.000000000000000000, 0.000000000000000000, 0.000000000000000000 ) ) ;
#9686=CARTESIAN_POINT ( 'NONE',  ( 4.071447262713884463, 2.020725942163681399, 3.499999999999996003 ) ) ;
#9716=CIRCLE ( 'NONE', #716, 5.371010071662839280 ) ;
#9722=( GEOMETRIC_REPRESENTATION_CONTEXT ( 3 ) GLOBAL_UNCERTAINTY_ASSIGNED_CONTEXT ( ( #22732 ) ) GLOBAL_UNIT_ASSIGNED_CONTEXT ( ( #4279, #19951, #656 ) ) REPRESENTATION_CONTEXT ( 'NONE', 'WORKASPACE' ) );
#9723=CARTESIAN_POINT ( 'NONE',  ( 4.170895651974849905, -4.109780709045238289, -6.938019423604825320E-15 ) ) ;
#9771=VERTEX_POINT ( 'NONE', #12656 ) ;
#9781=CARTESIAN_POINT ( 'NONE',  ( 0.1217565302851174314, 3.710888496608926612, -0.5725525826505064586 ) ) ;
#9810=CARTESIAN_POINT ( 'NONE',  ( 3.878089031707351086, 0.7015470581927514271, 3.499999999999968914 ) ) ;
#9819=ORIENTED_EDGE ( 'NONE', *, *, #20733, .F. ) ;
#9828=CARTESIAN_POINT ( 'NONE',  ( 4.093692494532773729, -2.021783646005764101, 3.501831996793847157 ) ) ;
#9940=EDGE_LOOP ( 'NONE', ( #9366, #686, #7589, #11312, #17042 ) ) ;
#9958=CARTESIAN_POINT ( 'NONE',  ( 4.165266963751721008, 2.049631966911937830, 3.550066703508936605 ) ) ;
#9980=( BOUNDED_SURFACE ( )  B_SPLINE_SURFACE ( 3, 2, ( 
 ( #12925, #3858, #233 ),
 ( #19983, #1863, #9402 ),
 ( #10808, #18226, #7518 ),
 ( #9280, #19873, #1750 ),
 ( #20103, #11156, #12575 ),
 ( #3976, #3745, #3641 ) ),
 .UNSPECIFIED., .F., .F., .F. ) 
 B_SPLINE_SURFACE_WITH_KNOTS ( ( 4, 2, 4 ),
 ( 3, 3 ),
 ( 0.01651999345535505245, 0.01858032176739835006, 0.02064065007944164420 ),
 ( 0.000000000000000000, 1.000000000000000000 ),
 .UNSPECIFIED. ) 
 GEOMETRIC_REPRESENTATION_ITEM ( )  RATIONAL_B_SPLINE_SURFACE ( (
 ( 1.000000000000000000, 0.8047781103519392465, 1.000000000000000000),
 ( 1.000000000000000000, 0.8123785825599156851, 1.000000000000000000),
 ( 1.000000000000000000, 0.8190671539795181255, 1.000000000000000000),
 ( 1.000000000000000000, 0.8192352254827984792, 1.000000000000000000),
 ( 1.000000000000000000, 0.8126129677216777925, 1.000000000000000000),
 ( 1.000000000000000000, 0.8047712537969735624, 1.000000000000000000) ) ) 
 REPRESENTATION_ITEM ( '' )  SURFACE ( )  );
#9993=CIRCLE ( 'NONE', #22767, 2.055000000000002380 ) ;
#10002=EDGE_LOOP ( 'NONE', ( #15792, #10652, #5264, #11639, #10992 ) ) ;
#10014=CARTESIAN_POINT ( 'NONE',  ( 0.3126073911696447549, 4.041451884327362798, -2.081668171172168513E-14 ) ) ;
#10018=EDGE_CURVE ( 'NONE', #4783, #12739, #19771, .T. ) ;
#10174=CARTESIAN_POINT ( 'NONE',  ( 0.02944718078429346339, -0.6813962075686514908, -3.500000000000035971 ) ) ;
#10175=DIRECTION ( 'NONE',  ( -3.204747427460357394E-31, 0.8660254037844378194, -0.5000000000000016653 ) ) ;
#10181=LINE ( 'NONE', #8653, #8692 ) ;
#10182=CARTESIAN_POINT ( 'NONE',  ( 0.000000000000000000, 0.000000000000000000, 0.000000000000000000 ) ) ;
#10197=ORIENTED_EDGE ( 'NONE', *, *, #13389, .T. ) ;
#10202=CARTESIAN_POINT ( 'NONE',  ( 3.972066048304726316, 3.435565134476395333, 1.180968096049722194 ) ) ;
#10229=CARTESIAN_POINT ( 'NONE',  ( 4.071447262713891568, -2.020725942163709377, -3.499999999999999556 ) ) ;
#10246=ORIENTED_EDGE ( 'NONE', *, *, #11116, .F. ) ;
#10247=UNCERTAINTY_MEASURE_WITH_UNIT (LENGTH_MEASURE( 1.000000000000000082E-05 ), #7825, 'distance_accuracy_value', 'NONE');
#10259=AXIS2_PLACEMENT_3D ( 'NONE', #14789, #18432, #18213 ) ;
#10293=FACE_OUTER_BOUND ( 'NONE', #19949, .T. ) ;
#10295=CARTESIAN_POINT ( 'NONE',  ( 4.071447262713891568, -4.041451884327432076, 1.040834085586084257E-14 ) ) ;
#10314=VECTOR ( 'NONE', #9225, 1000.000000000000000 ) ;
#10334=ORIENTED_EDGE ( 'NONE', *, *, #9120, .F. ) ;
#10381=CARTESIAN_POINT ( 'NONE',  ( 4.086376210449940594, 2.103254844323305228, 3.499999999999968026 ) ) ;
#10391=VERTEX_POINT ( 'NONE', #9578 ) ;
#10405=CIRCLE ( 'NONE', #7781, 5.200000000000008171 ) ;
#10422=VECTOR ( 'NONE', #6113, 1000.000000000000114 ) ;
#10477=CARTESIAN_POINT ( 'NONE',  ( 4.132952817037869764, 2.031684012687259955, -3.518979934899760131 ) ) ;
#10496=DIRECTION ( 'NONE',  ( -1.000000000000000000, -1.479114197289397135E-31, -5.916456789157588541E-31 ) ) ;
#10524=CARTESIAN_POINT ( 'NONE',  ( 0.02944718078671985234, -0.6813962075909525407, 3.499999999999960032 ) ) ;
#10533=CARTESIAN_POINT ( 'NONE',  ( 4.071447262713891568, 4.041451884327377009, -2.081668171172168513E-14 ) ) ;
#10582=CARTESIAN_POINT ( 'NONE',  ( 0.000000000000000000, 0.000000000000000000, 3.499999999999975131 ) ) ;
#10594=EDGE_LOOP ( 'NONE', ( #8295, #20887, #22829, #12157, #19936 ) ) ;
#10640=DIRECTION ( 'NONE',  ( 0.000000000000000000, 3.382522293539643228E-32, 1.000000000000000000 ) ) ;
#10652=ORIENTED_EDGE ( 'NONE', *, *, #2987, .T. ) ;
#10653=AXIS2_PLACEMENT_3D ( 'NONE', #15632, #22823, #13878 ) ;
#10654=STYLED_ITEM ( 'NONE', ( #17195 ), #12881 ) ;
#10694=ADVANCED_FACE ( 'NONE', ( #4096 ), #7746, .F. ) ;
#10695=PLANE ( 'NONE',  #12375 ) ;
#10703=CARTESIAN_POINT ( 'NONE',  ( 3.973110223765540017, 0.6902454861566492683, -3.565797985667426673 ) ) ;
#10706=CARTESIAN_POINT ( 'NONE',  ( 3.961551342854190860, -3.742715940867750835, 0.5174258321191379517 ) ) ;
#10732=APPLICATION_CONTEXT ( 'automotive_design' ) ;
#10808=CARTESIAN_POINT ( 'NONE',  ( 3.880206590543044953, -2.665671387532588366, -2.382921720511024244 ) ) ;
#10819=CARTESIAN_POINT ( 'NONE',  ( 4.082498951862917558, 2.020725942163638766, -3.499999999999997780 ) ) ;
#10871=CARTESIAN_POINT ( 'NONE',  ( 4.082498951862921999, -2.020725942163709377, -3.499999999999999556 ) ) ;
#10892=DIRECTION ( 'NONE',  ( -1.000000000000000000, -1.479114197289397135E-31, -5.916456789157588541E-31 ) ) ;
#10923=CARTESIAN_POINT ( 'NONE',  ( 3.880206590543190170, -3.396506438958537988, 1.117078279489006620 ) ) ;
#10989=DIRECTION ( 'NONE',  ( -1.000000000000000000, -1.479114197289397135E-31, -5.916456789157588541E-31 ) ) ;
#10992=ORIENTED_EDGE ( 'NONE', *, *, #4025, .F. ) ;
#11002=VERTEX_POINT ( 'NONE', #21844 ) ;
#11050=CARTESIAN_POINT ( 'NONE',  ( 4.158806965674309630, 4.075748668183996060, 0.05940377217582432784 ) ) ;
#11071=FACE_BOUND ( 'NONE', #16486, .T. ) ;
#11116=EDGE_CURVE ( 'NONE', #6445, #13557, #3191, .T. ) ;
#11156=CARTESIAN_POINT ( 'NONE',  ( 4.030867648405042303, -3.732851566701254953, -0.5345114293579096287 ) ) ;
#11185=CARTESIAN_POINT ( 'NONE',  ( 4.175326769692849993, 4.121399112977843338, -4.212005211934550870E-14 ) ) ;
#11198=B_SPLINE_CURVE_WITH_KNOTS ( 'NONE', 3,
 ( #18719, #9781, #16934, #847 ),
 .UNSPECIFIED., .F., .F.,
 ( 4, 4 ),
 ( 2.380739282476591411E-07, 0.002044882221487541018 ),
 .UNSPECIFIED. ) ;
#11238=ORIENTED_EDGE ( 'NONE', *, *, #7501, .F. ) ;
#11261=ADVANCED_FACE ( 'NONE', ( #10293 ), #21909, .T. ) ;
#11272=CARTESIAN_POINT ( 'NONE',  ( 2.023222897811621159E-14, -0.3420925509381568808, -3.500000000000033751 ) ) ;
#11279=CARTESIAN_POINT ( 'NONE',  ( 3.948103430091022492, 2.682758828852624067, -2.353325403973583807 ) ) ;
#11289=ORIENTED_EDGE ( 'NONE', *, *, #23179, .F. ) ;
#11312=ORIENTED_EDGE ( 'NONE', *, *, #20020, .F. ) ;
#11320=ORIENTED_EDGE ( 'NONE', *, *, #13548, .F. ) ;
#11321=CARTESIAN_POINT ( 'NONE',  ( 1.015987785799958376E-14, -3.202582148906756299, -1.452965002680425277 ) ) ;
#11325=CARTESIAN_POINT ( 'NONE',  ( 0.000000000000000000, 3.031088913245508110, -1.750000000000029310 ) ) ;
#11341=EDGE_LOOP ( 'NONE', ( #11837, #18127, #21356, #15880 ) ) ;
#11369=EDGE_CURVE ( 'NONE', #19811, #7132, #21979, .T. ) ;
#11370=EDGE_CURVE ( 'NONE', #1330, #7794, #14094, .T. ) ;
#11385=CARTESIAN_POINT ( 'NONE',  ( 25.15499999999999403, 0.000000000000000000, -6.938893903907228378E-15 ) ) ;
#11420=CARTESIAN_POINT ( 'NONE',  ( 0.000000000000000000, 3.031088913245536087, 1.749999999999998002 ) ) ;
#11439=ORIENTED_EDGE ( 'NONE', *, *, #14707, .T. ) ;
#11449=CARTESIAN_POINT ( 'NONE',  ( 4.033906725094494661, -1.419670120619062503, 3.499999999999970246 ) ) ;
#11462=AXIS2_PLACEMENT_3D ( 'NONE', #4560, #20932, #4800 ) ;
#11505=CARTESIAN_POINT ( 'NONE',  ( 3.950241966887847234, 3.393956070637395239, -1.121495646998965645 ) ) ;
#11513=ORIENTED_EDGE ( 'NONE', *, *, #20306, .F. ) ;
#11576=AXIS2_PLACEMENT_3D ( 'NONE', #6453, #8454, #21042 ) ;
#11584=CARTESIAN_POINT ( 'NONE',  ( 5.600000000000000533, 2.020725942163612121, 3.499999999999957812 ) ) ;
#11590=CARTESIAN_POINT ( 'NONE',  ( 4.082498951862915781, 2.020725942163681399, 3.499999999999996003 ) ) ;
#11601=CARTESIAN_POINT ( 'NONE',  ( 4.050880675075977599, -1.379097446046351649, -3.567934390854435645 ) ) ;
#11613=DIRECTION ( 'NONE',  ( -0.7071067811865530128, 8.659560562354856437E-17, -0.7071067811865421326 ) ) ;
#11639=ORIENTED_EDGE ( 'NONE', *, *, #1347, .F. ) ;
#11640=CARTESIAN_POINT ( 'NONE',  ( 4.071447262713891568, 4.041451884327377009, -2.081668171172168513E-14 ) ) ;
#11646=CIRCLE ( 'NONE', #6040, 5.371010071662839280 ) ;
#11664=CARTESIAN_POINT ( 'NONE',  ( 4.175813232069142344, 2.061359961916322980, 3.570380186727409200 ) ) ;
#11668=FILL_AREA_STYLE_COLOUR ( '', #7279 ) ;
#11695=CARTESIAN_POINT ( 'NONE',  ( 4.175075985190096262, -2.060370777630091244, 3.568666869285578969 ) ) ;
#11733=CARTESIAN_POINT ( 'NONE',  ( 4.055492966679525857, 2.385006769472625354, 3.005124364834308892 ) ) ;
#11777=ORIENTED_EDGE ( 'NONE', *, *, #20306, .T. ) ;
#11810=EDGE_LOOP ( 'NONE', ( #3555, #13851 ) ) ;
#11837=ORIENTED_EDGE ( 'NONE', *, *, #9531, .F. ) ;
#11843=ORIENTED_EDGE ( 'NONE', *, *, #2823, .T. ) ;
#11846=ADVANCED_FACE ( 'NONE', ( #11071, #3898 ), #19630, .T. ) ;
#11847=ORIENTED_EDGE ( 'NONE', *, *, #7675, .T. ) ;
#11873=EDGE_LOOP ( 'NONE', ( #21812, #11238 ) ) ;
#11913=VECTOR ( 'NONE', #17500, 1000.000000000000114 ) ;
#11924=EDGE_LOOP ( 'NONE', ( #19032, #1459, #18791, #9019 ) ) ;
#11934=CARTESIAN_POINT ( 'NONE',  ( 4.114405500665262672, 2.025575754679666662, 3.508400121684944750 ) ) ;
#11939=EDGE_CURVE ( 'NONE', #12509, #22096, #3504, .T. ) ;
#11971=ADVANCED_BREP_SHAPE_REPRESENTATION ( '', ( #12881, #22115 ), #2577 ) ;
#11978=ORIENTED_EDGE ( 'NONE', *, *, #19344, .T. ) ;
#11986=CARTESIAN_POINT ( 'NONE',  ( 0.3126073911695753660, -2.020725942163847932, -3.499999999999975131 ) ) ;
#11991=CARTESIAN_POINT ( 'NONE',  ( 3.951447005078450037, 1.347150628109081039, -3.499999999999995559 ) ) ;
#12069=CARTESIAN_POINT ( 'NONE',  ( 4.158806965674280320, 1.986429158307019938, 3.559403772175798952 ) ) ;
#12083=ORIENTED_EDGE ( 'NONE', *, *, #2199, .T. ) ;
#12090=FACE_OUTER_BOUND ( 'NONE', #2408, .T. ) ;
#12129=CARTESIAN_POINT ( 'NONE',  ( 4.050823680195217769, 2.400527758044860960, 2.978030508226152673 ) ) ;
#12154=AXIS2_PLACEMENT_3D ( 'NONE', #14918, #16781, #22803 ) ;
#12157=ORIENTED_EDGE ( 'NONE', *, *, #15485, .F. ) ;
#12169=CARTESIAN_POINT ( 'NONE',  ( 3.951447005078448260, -2.357513599190994125, 2.916666666666669183 ) ) ;
#12223=CARTESIAN_POINT ( 'NONE',  ( 3.958484000407217707, -2.327740518749036092, 2.968235154689960797 ) ) ;
#12322=B_SPLINE_CURVE_WITH_KNOTS ( 'NONE', 3,
 ( #18340, #11272, #10174, #22771, #16550, #13826 ),
 .UNSPECIFIED., .F., .F.,
 ( 4, 2, 4 ),
 ( 0.01308430721348209473, 0.01410661710602284513, 0.01512892699856359380 ),
 .UNSPECIFIED. ) ;
#12348=DIRECTION ( 'NONE',  ( 0.000000000000000000, 3.382522293539642681E-32, 1.000000000000000000 ) ) ;
#12372=CARTESIAN_POINT ( 'NONE',  ( 5.600000000000000533, -2.020725942163709377, -3.500000000000010214 ) ) ;
#12375=AXIS2_PLACEMENT_3D ( 'NONE', #9171, #17878, #7181 ) ;
#12401=EDGE_CURVE ( 'NONE', #6728, #927, #12670, .T. ) ;
#12427=EDGE_CURVE ( 'NONE', #6445, #15071, #3005, .T. ) ;
#12451=CARTESIAN_POINT ( 'NONE',  ( 1.848892746611746769E-30, 8.456305733849119291E-32, 2.500000000000003997 ) ) ;
#12452=CARTESIAN_POINT ( 'NONE',  ( 0.000000000000000000, 3.031088913245536087, 1.749999999999998002 ) ) ;
#12484=CARTESIAN_POINT ( 'NONE',  ( 4.071447262713891568, -4.041451884327432076, 1.040834085586084257E-14 ) ) ;
#12509=VERTEX_POINT ( 'NONE', #13480 ) ;
#12546=VECTOR ( 'NONE', #20664, 1000.000000000000000 ) ;
#12548=CARTESIAN_POINT ( 'NONE',  ( 4.050536630291712292, -3.778525289263205078, -0.5912575323400444116 ) ) ;
#12573=DIRECTION ( 'NONE',  ( 1.133987551255203069E-30, -2.220446049250310616E-16, 1.000000000000000000 ) ) ;
#12575=CARTESIAN_POINT ( 'NONE',  ( 4.052424581287677796, -3.786734753435081480, -0.5771415817958118755 ) ) ;
#12586=CARTESIAN_POINT ( 'NONE',  ( 4.165266963751722784, 2.049631966912018211, -3.550066703508910848 ) ) ;
#12587=CARTESIAN_POINT ( 'NONE',  ( 3.950241966887848122, -3.393956070637773603, 1.121495646999037143 ) ) ;
#12601=CARTESIAN_POINT ( 'NONE',  ( 0.000000000000000000, 0.000000000000000000, 0.000000000000000000 ) ) ;
#12619=EDGE_LOOP ( 'NONE', ( #21112, #4729, #7174, #2325, #22853, #19631, #7594 ) ) ;
#12656=CARTESIAN_POINT ( 'NONE',  ( 4.175813232069149450, 2.061359961916364725, -3.570380186727398986 ) ) ;
#12670=B_SPLINE_CURVE_WITH_KNOTS ( 'NONE', 3,
 ( #664, #18649, #9828, #1134, #6306, #4403, #8299, #15457, #900, #7833, #15347, #6422, #11695, #8062, #20889, #13593 ),
 .UNSPECIFIED., .F., .F.,
 ( 4, 3, 3, 3, 3, 4 ),
 ( 0.000000000000000000, 3.315506744709602110E-05, 6.608280158699779622E-05, 0.0001026520855291460272, 0.0001376952025664770357, 0.0001398064759190588782 ),
 .UNSPECIFIED. ) ;
#12684=ADVANCED_FACE ( 'NONE', ( #19224 ), #19705, .F. ) ;
#12704=CARTESIAN_POINT ( 'NONE',  ( 4.175326769692856210, 2.060699556488918560, -3.569236330973474924 ) ) ;
#12729=CONICAL_SURFACE ( 'NONE', #5236, 3.500000000000004441, 1.047197551196600296 ) ;
#12739=VERTEX_POINT ( 'NONE', #1813 ) ;
#12749=ORIENTED_EDGE ( 'NONE', *, *, #2867, .T. ) ;
#12788=CARTESIAN_POINT ( 'NONE',  ( 4.071447262713884463, 2.020725942163681399, 3.499999999999996003 ) ) ;
#12805=CARTESIAN_POINT ( 'NONE',  ( 3.972709601346602337, 2.746729940827207894, -2.374099244652752461 ) ) ;
#12815=CARTESIAN_POINT ( 'NONE',  ( 4.030867648405429549, 2.329326259789358922, -2.965488570641425792 ) ) ;
#12818=EDGE_CURVE ( 'NONE', #7794, #9067, #18176, .T. ) ;
#12839=FACE_OUTER_BOUND ( 'NONE', #771, .T. ) ;
#12855=ORIENTED_EDGE ( 'NONE', *, *, #10018, .F. ) ;
#12856=EDGE_CURVE ( 'NONE', #6445, #14430, #296, .T. ) ;
#12881=MANIFOLD_SOLID_BREP ( 'FlangeHexFillet', #3556 ) ;
#12882=SURFACE_STYLE_USAGE ( .BOTH. , #16626 ) ;
#12925=CARTESIAN_POINT ( 'NONE',  ( 4.086262629614044073, -1.979770830881117494, -3.570936333571148591 ) ) ;
#12930=LINE ( 'NONE', #7185, #429 ) ;
#12994=CARTESIAN_POINT ( 'NONE',  ( 4.175572532730935649, -2.061029303918082256, -3.569807470274393602 ) ) ;
#13032=CARTESIAN_POINT ( 'NONE',  ( 4.033895293472003374, 1.419609371826466848, -3.500000000000009326 ) ) ;
#13053=CARTESIAN_POINT ( 'NONE',  ( 3.974175853610000253, 3.450041667725515460, -1.156004144284047630 ) ) ;
#13111=CARTESIAN_POINT ( 'NONE',  ( 3.961557105775345367, -1.423285172353660144, 3.499999999999970246 ) ) ;
#13132=EDGE_LOOP ( 'NONE', ( #21446, #13266, #11439, #13727 ) ) ;
#13188=CARTESIAN_POINT ( 'NONE',  ( 4.132952817037863547, 4.063368025374519910, 3.469446951953614189E-15 ) ) ;
#13197=CARTESIAN_POINT ( 'NONE',  ( 0.000000000000000000, -3.031088913245480576, 1.749999999999994671 ) ) ;
#13221=CARTESIAN_POINT ( 'NONE',  ( 3.880214671983721608, -0.7309020039786100487, 3.499999999999969802 ) ) ;
#13246=CARTESIAN_POINT ( 'NONE',  ( 4.104070371397483541, 2.023683613428320260, 3.505122836902515360 ) ) ;
#13253=AXIS2_PLACEMENT_3D ( 'NONE', #2508, #16850, #5934 ) ;
#13261=CARTESIAN_POINT ( 'NONE',  ( 3.878104551856319748, -0.7018542299753877112, -3.500000000000009770 ) ) ;
#13266=ORIENTED_EDGE ( 'NONE', *, *, #16727, .T. ) ;
#13288=CARTESIAN_POINT ( 'NONE',  ( 4.055492966679612010, 3.795017426214636114, -0.5629142681440425511 ) ) ;
#13309=CARTESIAN_POINT ( 'NONE',  ( 4.175572532730939201, 4.122058607836078359, -4.513569816216541579E-15 ) ) ;
#13361=EDGE_CURVE ( 'NONE', #22096, #12509, #7500, .T. ) ;
#13365=ORIENTED_EDGE ( 'NONE', *, *, #3996, .F. ) ;
#13381=EDGE_LOOP ( 'NONE', ( #2086, #17006, #655, #5577, #8239 ) ) ;
#13386=VERTEX_POINT ( 'NONE', #5420 ) ;
#13389=EDGE_CURVE ( 'NONE', #15071, #16509, #17655, .T. ) ;
#13391=CARTESIAN_POINT ( 'NONE',  ( 4.086262629614002329, 1.979770830881015575, 3.570936333571067767 ) ) ;
#13392=ADVANCED_FACE ( 'NONE', ( #3533 ), #10695, .F. ) ;
#13437=ORIENTED_EDGE ( 'NONE', *, *, #13548, .T. ) ;
#13442=AXIS2_PLACEMENT_3D ( 'NONE', #651, #7587, #9587 ) ;
#13444=ORIENTED_EDGE ( 'NONE', *, *, #2047, .T. ) ;
#13480=CARTESIAN_POINT ( 'NONE',  ( 5.600000000000000533, 2.359070914220255805E-30, 2.499999999999996891 ) ) ;
#13548=EDGE_CURVE ( 'NONE', #10391, #9067, #12322, .T. ) ;
#13557=VERTEX_POINT ( 'NONE', #1707 ) ;
#13593=CARTESIAN_POINT ( 'NONE',  ( 4.175813232069142344, -2.061359961916364725, 3.570380186727402538 ) ) ;
#13619=PRODUCT_DEFINITION_SHAPE ( 'NONE', 'NONE',  #9348 ) ;
#13636=CARTESIAN_POINT ( 'NONE',  ( 4.071447262713884463, 2.020725942163639655, -3.499999999999996003 ) ) ;
#13682=DIRECTION ( 'NONE',  ( 1.000000000000000000, 1.479114197289397135E-31, 5.916456789157588541E-31 ) ) ;
#13693=CARTESIAN_POINT ( 'NONE',  ( 3.958491816110800254, 1.406739583088997048, 3.499999999999968470 ) ) ;
#13727=ORIENTED_EDGE ( 'NONE', *, *, #14038, .F. ) ;
#13747=CARTESIAN_POINT ( 'NONE',  ( 3.950241966887813483, 2.668221755853961596, 2.378504353000647331 ) ) ;
#13758=ORIENTED_EDGE ( 'NONE', *, *, #2867, .F. ) ;
#13826=CARTESIAN_POINT ( 'NONE',  ( 0.3126073911695753660, -2.020725942163847932, -3.499999999999975131 ) ) ;
#13831=CYLINDRICAL_SURFACE ( 'NONE', #1375, 2.500000000000003997 ) ;
#13834=DIRECTION ( 'NONE',  ( 1.000000000000000000, 1.479114197289397135E-31, 5.916456789157588541E-31 ) ) ;
#13851=ORIENTED_EDGE ( 'NONE', *, *, #16727, .F. ) ;
#13857=CARTESIAN_POINT ( 'NONE',  ( 4.180345304246171345, 4.135116856707326427, -0.02129519942693453363 ) ) ;
#13874=DIRECTION ( 'NONE',  ( -1.000000000000000000, -1.479114197289397135E-31, -5.916456789157588541E-31 ) ) ;
#13878=DIRECTION ( 'NONE',  ( -7.395570986446975166E-31, -3.382522293539642681E-32, -1.000000000000000000 ) ) ;
#13905=DIRECTION ( 'NONE',  ( -1.000000000000000000, -1.479114197289397135E-31, -5.916456789157588541E-31 ) ) ;
#13906=( NAMED_UNIT ( * ) SI_UNIT ( $, .STERADIAN. ) SOLID_ANGLE_UNIT ( ) );
#13960=CARTESIAN_POINT ( 'NONE',  ( 0.02993401039715783488, -2.688325911136484336, 2.343682934607788315 ) ) ;
#13989=VECTOR ( 'NONE', #11613, 999.9999999999998863 ) ;
#14038=EDGE_CURVE ( 'NONE', #20382, #15390, #11646, .T. ) ;
#14081=ORIENTED_EDGE ( 'NONE', *, *, #5371, .F. ) ;
#14088=CARTESIAN_POINT ( 'NONE',  ( 4.175813232069142344, 2.061359961916322980, 3.570380186727409200 ) ) ;
#14094=B_SPLINE_CURVE_WITH_KNOTS ( 'NONE', 3,
 ( #411, #12994, #18514, #16387, #7355, #18402, #2048, #21599, #5476, #9232, #5937, #3701, #19821, #4152, #10871, #22049 ),
 .UNSPECIFIED., .F., .F.,
 ( 4, 3, 3, 3, 3, 4 ),
 ( -2.111273352554612095E-06, 0.000000000000000000, 3.519286887797705194E-05, 7.191842652069450729E-05, 0.0001049868727093782207, 0.0001382836236822282622 ),
 .UNSPECIFIED. ) ;
#14141=LINE ( 'NONE', #21329, #23113 ) ;
#14213=LINE ( 'NONE', #15955, #20224 ) ;
#14234=CARTESIAN_POINT ( 'NONE',  ( 5.600000000000000533, 0.000000000000000000, -3.469446951953614189E-15 ) ) ;
#14237=B_SPLINE_CURVE_WITH_KNOTS ( 'NONE', 3,
 ( #22958, #10703, #17644, #5298 ),
 .UNSPECIFIED., .F., .F.,
 ( 4, 4 ),
 ( 0.002080789711329285828, 0.004173039763574515164 ),
 .UNSPECIFIED. ) ;
#14298=CARTESIAN_POINT ( 'NONE',  ( 3.806834918298653392, -3.031088913245548966, 1.749999999999996003 ) ) ;
#14337=CARTESIAN_POINT ( 'NONE',  ( 5.600000000000000533, 2.020725942163695166, -3.500000000000034195 ) ) ;
#14345=DIRECTION ( 'NONE',  ( -1.000000000000000000, -1.479114197289397135E-31, -5.916456789157588541E-31 ) ) ;
#14386=CARTESIAN_POINT ( 'NONE',  ( 5.600000000000000533, 3.061616997868409765E-16, -2.500000000000003997 ) ) ;
#14413=CARTESIAN_POINT ( 'NONE',  ( 1.448045174978588829E-14, 2.859595677584339857, -2.047034997319622018 ) ) ;
#14430=VERTEX_POINT ( 'NONE', #8246 ) ;
#14440=CARTESIAN_POINT ( 'NONE',  ( 4.175813232069149450, -2.061359961916378492, -3.570380186727402538 ) ) ;
#14454=AXIS2_PLACEMENT_3D ( 'NONE', #9684, #13682, #2730 ) ;
#14476=CARTESIAN_POINT ( 'NONE',  ( 3.974175853610087739, -3.450041667725798344, 1.156004144284031199 ) ) ;
#14480=ORIENTED_EDGE ( 'NONE', *, *, #17393, .F. ) ;
#14534=ORIENTED_EDGE ( 'NONE', *, *, #1347, .T. ) ;
#14650=ORIENTED_EDGE ( 'NONE', *, *, #20020, .T. ) ;
#14671=CARTESIAN_POINT ( 'NONE',  ( 3.974167765203684866, 0.7238254970431058366, -3.565825589389272743 ) ) ;
#14672=EDGE_CURVE ( 'NONE', #11002, #22096, #12930, .T. ) ;
#14681=CARTESIAN_POINT ( 'NONE',  ( 4.050536630291690088, 2.401306687817042373, -2.976670123173763116 ) ) ;
#14705=FACE_OUTER_BOUND ( 'NONE', #16487, .T. ) ;
#14707=EDGE_CURVE ( 'NONE', #1571, #15390, #6811, .T. ) ;
#14755=CARTESIAN_POINT ( 'NONE',  ( 0.2182387239031300108, 1.693823289467299098, -3.500000000000034639 ) ) ;
#14763=B_SPLINE_CURVE_WITH_KNOTS ( 'NONE', 3,
 ( #15430, #17540, #17192, #6501, #12129, #11664 ),
 .UNSPECIFIED., .F., .F.,
 ( 4, 2, 4 ),
 ( 0.000000000000000000, 0.002086519881787258883, 0.004173039763574517766 ),
 .UNSPECIFIED. ) ;
#14789=CARTESIAN_POINT ( 'NONE',  ( 0.000000000000000000, 0.000000000000000000, 0.000000000000000000 ) ) ;
#14812=B_SPLINE_CURVE_WITH_KNOTS ( 'NONE', 3,
 ( #19861, #8926, #21524, #19625, #21285, #7392 ),
 .UNSPECIFIED., .F., .F.,
 ( 4, 2, 4 ),
 ( 0.000000000000000000, 0.002086519881787257148, 0.004173039763574514296 ),
 .UNSPECIFIED. ) ;
#14830=DIRECTION ( 'NONE',  ( 1.000000000000000000, 1.479114197289397135E-31, 5.916456789157588541E-31 ) ) ;
#14839=PLANE ( 'NONE',  #8048 ) ;
#14880=( NAMED_UNIT ( * ) PLANE_ANGLE_UNIT ( ) SI_UNIT ( $, .RADIAN. ) );
#14891=CARTESIAN_POINT ( 'NONE',  ( 5.600000000000000533, -4.041451884327432076, -6.938893903907228378E-15 ) ) ;
#14918=CARTESIAN_POINT ( 'NONE',  ( 5.600000000000000533, 2.020725942163695166, -3.500000000000034195 ) ) ;
#14948=CARTESIAN_POINT ( 'NONE',  ( 0.000000000000000000, 4.041451884327362798, -2.081668171172168513E-14 ) ) ;
#14954=CARTESIAN_POINT ( 'NONE',  ( 25.60000000000000142, 6.951083313223974888E-32, 2.054999999999995719 ) ) ;
#15003=CARTESIAN_POINT ( 'NONE',  ( 4.165266963751720120, -4.099263933824012440, -2.757781224018043175E-14 ) ) ;
#15031=DIRECTION ( 'NONE',  ( -1.000000000000000000, -1.479114197289397135E-31, -5.916456789157588541E-31 ) ) ;
#15071=VERTEX_POINT ( 'NONE', #16185 ) ;
#15112=CARTESIAN_POINT ( 'NONE',  ( 4.114405500665258231, -4.051151509359430136, -3.718102049540426238E-17 ) ) ;
#15114=CARTESIAN_POINT ( 'NONE',  ( 4.093692494532772841, 2.021783646005722801, 3.501831996793851154 ) ) ;
#15144=CARTESIAN_POINT ( 'NONE',  ( 25.60000000000000142, 2.516649172247813527E-16, -2.055000000000009486 ) ) ;
#15217=ORIENTED_EDGE ( 'NONE', *, *, #2987, .F. ) ;
#15302=AXIS2_PLACEMENT_3D ( 'NONE', #11385, #15031, #22220 ) ;
#15319=SURFACE_SIDE_STYLE ('',( #8152 ) ) ;
#15347=CARTESIAN_POINT ( 'NONE',  ( 4.165266963751715679, -2.049631966912040415, 3.550066703508925059 ) ) ;
#15390=VERTEX_POINT ( 'NONE', #7441 ) ;
#15429=VERTEX_POINT ( 'NONE', #18482 ) ;
#15430=CARTESIAN_POINT ( 'NONE',  ( 4.175813232069149450, 4.122719923832687705, 1.040834085586084257E-14 ) ) ;
#15433=( LENGTH_UNIT ( ) NAMED_UNIT ( * ) SI_UNIT ( .MILLI., .METRE. ) );
#15441=DIRECTION ( 'NONE',  ( -7.395570986446975166E-31, -3.382522293539642681E-32, -1.000000000000000000 ) ) ;
#15457=CARTESIAN_POINT ( 'NONE',  ( 4.142654963991867056, -2.035398498734353190, 3.525413613457324402 ) ) ;
#15471=FACE_OUTER_BOUND ( 'NONE', #17126, .T. ) ;
#15476=CARTESIAN_POINT ( 'NONE',  ( 3.973110223767149840, -2.262799480050941678E-11, -3.565797985667468417 ) ) ;
#15485=EDGE_CURVE ( 'NONE', #16509, #1004, #9640, .T. ) ;
#15504=CARTESIAN_POINT ( 'NONE',  ( 3.973110223765516036, -0.6902454861566473809, 3.565797985667351622 ) ) ;
#15611=CARTESIAN_POINT ( 'NONE',  ( 0.000000000000000000, -3.031088913245480576, 1.749999999999994671 ) ) ;
#15632=CARTESIAN_POINT ( 'NONE',  ( 0.000000000000000000, 0.000000000000000000, 0.000000000000000000 ) ) ;
#15666=CARTESIAN_POINT ( 'NONE',  ( 4.052432342741398408, 1.393590342654249525, 3.567979436357390011 ) ) ;
#15741=CIRCLE ( 'NONE', #4477, 2.500000000000003997 ) ;
#15751=FACE_OUTER_BOUND ( 'NONE', #19783, .T. ) ;
#15792=ORIENTED_EDGE ( 'NONE', *, *, #12818, .F. ) ;
#15813=CARTESIAN_POINT ( 'NONE',  ( 3.951447005078454477, 3.704664227300094481, -0.5833333333333537984 ) ) ;
#15851=ORIENTED_EDGE ( 'NONE', *, *, #3077, .T. ) ;
#15868=CARTESIAN_POINT ( 'NONE',  ( 4.180345304246196214, -2.049116244671368658, 3.591763845239293484 ) ) ;
#15880=ORIENTED_EDGE ( 'NONE', *, *, #2635, .F. ) ;
#15939=DIRECTION ( 'NONE',  ( -1.000000000000000000, -1.479114197289397135E-31, -5.916456789157588541E-31 ) ) ;
#15955=CARTESIAN_POINT ( 'NONE',  ( 5.600000000000000533, 4.041451884327335264, -1.734723475976807094E-14 ) ) ;
#15976=DIRECTION ( 'NONE',  ( -1.000000000000000000, -1.479114197289397135E-31, -5.916456789157588541E-31 ) ) ;
#15991=CARTESIAN_POINT ( 'NONE',  ( 5.600000000000000533, 0.000000000000000000, -3.469446951953614189E-15 ) ) ;
#16005=EDGE_CURVE ( 'NONE', #6667, #4783, #20015, .T. ) ;
#16012=CARTESIAN_POINT ( 'NONE',  ( 4.630153689607049650, 0.000000000000000000, -3.469446951953614189E-15 ) ) ;
#16027=ORIENTED_EDGE ( 'NONE', *, *, #5371, .T. ) ;
#16092=CARTESIAN_POINT ( 'NONE',  ( 4.175813232069149450, 4.122719923832687705, 1.040834085586084257E-14 ) ) ;
#16095=CARTESIAN_POINT ( 'NONE',  ( 0.1397371499201390255, 1.362866705336802875, 3.499999999999957812 ) ) ;
#16100=CARTESIAN_POINT ( 'NONE',  ( 4.175075985190096262, 2.060370777630105010, -3.568666869285575860 ) ) ;
#16101=CARTESIAN_POINT ( 'NONE',  ( 4.030867648404789172, -2.329326259789488596, 2.965488570641482191 ) ) ;
#16147=EDGE_LOOP ( 'NONE', ( #17786, #15217, #21620, #17956 ) ) ;
#16158=CARTESIAN_POINT ( 'NONE',  ( 3.951447005078452701, -3.704664227300147328, 0.5833333333333443615 ) ) ;
#16185=CARTESIAN_POINT ( 'NONE',  ( 0.3126073911696378160, 2.020725942163612121, 3.499999999999975131 ) ) ;
#16215=CARTESIAN_POINT ( 'NONE',  ( 4.104070371397483541, 2.023683613428375772, -3.505122836902498040 ) ) ;
#16216=CARTESIAN_POINT ( 'NONE',  ( 0.000000000000000000, -3.031088913245536087, -1.750000000000001554 ) ) ;
#16245=EDGE_CURVE ( 'NONE', #17692, #1330, #22521, .T. ) ;
#16247=AXIS2_PLACEMENT_3D ( 'NONE', #16896, #8088, #2911 ) ;
#16304=EDGE_CURVE ( 'NONE', #17692, #19662, #652, .T. ) ;
#16329=CARTESIAN_POINT ( 'NONE',  ( 0.1217565302850851516, 2.351289329882099821, 2.927447417349521963 ) ) ;
#16334=CARTESIAN_POINT ( 'NONE',  ( -2.351786978051564260E-14, 0.3423821193870958401, 3.499999999999959588 ) ) ;
#16340=CARTESIAN_POINT ( 'NONE',  ( 4.180231891692622881, 4.134807952925586783, 0.02076457676759232637 ) ) ;
#16371=ADVANCED_FACE ( 'NONE', ( #558 ), #7720, .F. ) ;
#16387=CARTESIAN_POINT ( 'NONE',  ( 4.175075985190096262, -2.060370777630243566, -3.568666869285537668 ) ) ;
#16388=CARTESIAN_POINT ( 'NONE',  ( 3.806834918298672488, -3.031088913245592043, -1.750000000000008438 ) ) ;
#16425=DIRECTION ( 'NONE',  ( -1.000000000000000000, -1.479114197289397135E-31, -5.916456789157588541E-31 ) ) ;
#16451=CARTESIAN_POINT ( 'NONE',  ( 4.158921614371308806, 1.986121848748776175, -3.559936047944516346 ) ) ;
#16471=CARTESIAN_POINT ( 'NONE',  ( 4.151274195509691012, 4.079825909417423624, 3.209661024741434261E-15 ) ) ;
#16486=EDGE_LOOP ( 'NONE', ( #18800, #18395 ) ) ;
#16487=EDGE_LOOP ( 'NONE', ( #7032, #8669, #19104, #16834 ) ) ;
#16490=ORIENTED_EDGE ( 'NONE', *, *, #1852, .T. ) ;
#16509=VERTEX_POINT ( 'NONE', #22658 ) ;
#16537=CARTESIAN_POINT ( 'NONE',  ( 3.961545574370043177, 1.423222908133018549, -3.500000000000009326 ) ) ;
#16550=CARTESIAN_POINT ( 'NONE',  ( 0.2175679805370102360, -1.691499766289419782, -3.500000000000035527 ) ) ;
#16571=CYLINDRICAL_SURFACE ( 'NONE', #2450, 2.500000000000003997 ) ;
#16574=CARTESIAN_POINT ( 'NONE',  ( 4.142654963991841299, 4.070796997468685063, 3.571802849091299743E-15 ) ) ;
#16595=UNCERTAINTY_MEASURE_WITH_UNIT (LENGTH_MEASURE( 1.000000000000000082E-05 ), #15433, 'distance_accuracy_value', 'NONE');
#16616=CARTESIAN_POINT ( 'NONE',  ( 4.071447262713891568, -4.041451884327432076, 1.040834085586084257E-14 ) ) ;
#16617=CARTESIAN_POINT ( 'NONE',  ( 4.158806752148092478, -2.089318365061886951, 3.499999999999970246 ) ) ;
#16626=SURFACE_SIDE_STYLE ('',( #18639 ) ) ;
#16727=EDGE_CURVE ( 'NONE', #15429, #1571, #115, .T. ) ;
#16742=CARTESIAN_POINT ( 'NONE',  ( 0.1397371499203269585, 1.362866705341221785, -3.500000000000035083 ) ) ;
#16766=DIRECTION ( 'NONE',  ( 0.000000000000000000, 3.382522293539643228E-32, 1.000000000000000000 ) ) ;
#16781=DIRECTION ( 'NONE',  ( 3.759415251443883509E-31, -0.8660254037844378194, 0.5000000000000014433 ) ) ;
#16788=CARTESIAN_POINT ( 'NONE',  ( 3.961551342854520819, 3.742715940867734847, -0.5174258321191672616 ) ) ;
#16834=ORIENTED_EDGE ( 'NONE', *, *, #13361, .F. ) ;
#16841=CARTESIAN_POINT ( 'NONE',  ( 4.071447262713891568, 4.041451884327377009, -2.081668171172168513E-14 ) ) ;
#16850=DIRECTION ( 'NONE',  ( -1.000000000000000000, -1.479114197289397135E-31, -5.916456789157588541E-31 ) ) ;
#16856=COLOUR_RGB ( '', 0.66274510, 0.83137255, 0.94901961) ;
#16877=CARTESIAN_POINT ( 'NONE',  ( 4.132952817037863547, -4.063368025374519910, 2.081668171172168513E-14 ) ) ;
#16896=CARTESIAN_POINT ( 'NONE',  ( 25.60000000000000142, 0.000000000000000000, -6.938893903907228378E-15 ) ) ;
#16934=CARTESIAN_POINT ( 'NONE',  ( 8.529852775121097885E-15, 3.375361811986506755, -1.153701847711674278 ) ) ;
#16936=CARTESIAN_POINT ( 'NONE',  ( 1.789509255758340803E-14, -3.375361811986531180, 1.153701847711657846 ) ) ;
#16954=CARTESIAN_POINT ( 'NONE',  ( 0.3126073911696447549, -4.041451884327432076, 3.469446951953614189E-15 ) ) ;
#16992=DIRECTION ( 'NONE',  ( -7.395570986446975166E-31, -3.382522293539642681E-32, -1.000000000000000000 ) ) ;
#17006=ORIENTED_EDGE ( 'NONE', *, *, #3996, .T. ) ;
#17018=AXIS2_PLACEMENT_3D ( 'NONE', #1298, #1404, #3635 ) ;
#17042=ORIENTED_EDGE ( 'NONE', *, *, #7627, .F. ) ;
#17074=FILL_AREA_STYLE ('',( #11668 ) ) ;
#17126=EDGE_LOOP ( 'NONE', ( #1353, #8343, #5201 ) ) ;
#17192=CARTESIAN_POINT ( 'NONE',  ( 3.972709601346574360, 3.429395227388265521, 1.191688283765287348 ) ) ;
#17195=PRESENTATION_STYLE_ASSIGNMENT (( #22510 ) ) ;
#17196=DIRECTION ( 'NONE',  ( -1.000000000000000000, -1.479114197289397135E-31, -5.916456789157588541E-31 ) ) ;
#17240=CARTESIAN_POINT ( 'NONE',  ( 0.000000000000000000, 0.000000000000000000, 0.000000000000000000 ) ) ;
#17315=DIRECTION ( 'NONE',  ( 0.000000000000000000, -1.224646799147353947E-16, 1.000000000000000000 ) ) ;
#17371=CARTESIAN_POINT ( 'NONE',  ( 3.958484000407108461, 3.734437307742041412, 0.5317648453098983152 ) ) ;
#17393=EDGE_CURVE ( 'NONE', #6728, #6445, #3968, .T. ) ;
#17398=CARTESIAN_POINT ( 'NONE',  ( 3.806834918298644066, -3.469446951953614189E-14, -3.500000000000012434 ) ) ;
#17493=FACE_OUTER_BOUND ( 'NONE', #19835, .T. ) ;
#17500=DIRECTION ( 'NONE',  ( 0.3420201433256618850, 1.150791560227853967E-16, 0.9396926207859108704 ) ) ;
#17507=DIRECTION ( 'NONE',  ( 0.000000000000000000, -3.382522293539642133E-32, -1.000000000000000000 ) ) ;
#17540=CARTESIAN_POINT ( 'NONE',  ( 4.050536630291722062, 3.778525289263191311, 0.5912575323400045546 ) ) ;
#17583=CARTESIAN_POINT ( 'NONE',  ( 25.60000000000000142, 0.000000000000000000, -6.938893903907228378E-15 ) ) ;
#17638=VERTEX_POINT ( 'NONE', #6228 ) ;
#17644=CARTESIAN_POINT ( 'NONE',  ( 4.050480423730739687, 1.376911654797406515, -3.567926555162024282 ) ) ;
#17645=CARTESIAN_POINT ( 'NONE',  ( 4.175813232069149450, 2.061359961916364725, -3.570380186727398986 ) ) ;
#17655=B_SPLINE_CURVE_WITH_KNOTS ( 'NONE', 3,
 ( #19874, #16329, #1752, #12452 ),
 .UNSPECIFIED., .F., .F.,
 ( 4, 4 ),
 ( 2.380739281923877002E-07, 0.002044882221487566605 ),
 .UNSPECIFIED. ) ;
#17668=DIRECTION ( 'NONE',  ( 6.409494854920715664E-31, 0.8660254037844388186, 0.4999999999999997224 ) ) ;
#17690=CARTESIAN_POINT ( 'NONE',  ( -2.306216605489283533E-14, -0.3420925509533392916, 3.499999999999959588 ) ) ;
#17692=VERTEX_POINT ( 'NONE', #3932 ) ;
#17701=FACE_OUTER_BOUND ( 'NONE', #1493, .T. ) ;
#17786=ORIENTED_EDGE ( 'NONE', *, *, #16304, .T. ) ;
#17819=VERTEX_POINT ( 'NONE', #7815 ) ;
#17878=DIRECTION ( 'NONE',  ( -1.000000000000000000, -1.479114197289397135E-31, 7.395570986446975166E-31 ) ) ;
#17883=ADVANCED_FACE ( 'NONE', ( #20525 ), #7433, .F. ) ;
#17884=DIRECTION ( 'NONE',  ( 1.000000000000000000, 1.479114197289397573E-31, 0.000000000000000000 ) ) ;
#17891=CARTESIAN_POINT ( 'NONE',  ( 4.055492966679551614, -3.795017426214470913, 0.5629142681440486573 ) ) ;
#17899=B_SPLINE_CURVE_WITH_KNOTS ( 'NONE', 3,
 ( #8439, #11601, #19130, #15476 ),
 .UNSPECIFIED., .F., .F.,
 ( 4, 4 ),
 ( 0.000000000000000000, 0.002080789711329285828 ),
 .UNSPECIFIED. ) ;
#17956=ORIENTED_EDGE ( 'NONE', *, *, #16245, .F. ) ;
#17971=VECTOR ( 'NONE', #15939, 1000.000000000000000 ) ;
#17994=CIRCLE ( 'NONE', #5974, 2.055000000000002380 ) ;
#18002=EDGE_LOOP ( 'NONE', ( #19339, #725, #19605, #10246, #14480 ) ) ;
#18011=CARTESIAN_POINT ( 'NONE',  ( 4.158806965674314071, -4.075748668184007606, -0.05940377217584739272 ) ) ;
#18097=ORIENTED_EDGE ( 'NONE', *, *, #4081, .F. ) ;
#18104=CARTESIAN_POINT ( 'NONE',  ( 4.050823680195225762, 3.779313952391327280, -0.5899027668435032901 ) ) ;
#18127=ORIENTED_EDGE ( 'NONE', *, *, #7501, .T. ) ;
#18165=ADVANCED_FACE ( 'NONE', ( #18379 ), #7662, .T. ) ;
#18176=LINE ( 'NONE', #285, #10314 ) ;
#18213=DIRECTION ( 'NONE',  ( -7.395570986446975166E-31, -3.382522293539642681E-32, -1.000000000000000000 ) ) ;
#18226=CARTESIAN_POINT ( 'NONE',  ( 3.950241966887857004, -2.668221755853800392, -2.378504353000562066 ) ) ;
#18257=B_SPLINE_CURVE_WITH_KNOTS ( 'NONE', 3,
 ( #11640, #4004, #2702, #22126, #20255, #7663, #13188, #16574, #16471, #20360, #726, #7547, #6131, #11185, #13309, #20489 ),
 .UNSPECIFIED., .F., .F.,
 ( 4, 3, 3, 3, 3, 4 ),
 ( 0.000000000000000000, 3.315506744709154877E-05, 6.608280158698813327E-05, 0.0001026520855291333285, 0.0001376952025664795293, 0.0001398064759190609924 ),
 .UNSPECIFIED. ) ;
#18340=CARTESIAN_POINT ( 'NONE',  ( 0.000000000000000000, 0.000000000000000000, -3.499999999999996003 ) ) ;
#18379=FACE_OUTER_BOUND ( 'NONE', #20422, .T. ) ;
#18395=ORIENTED_EDGE ( 'NONE', *, *, #13361, .T. ) ;
#18402=CARTESIAN_POINT ( 'NONE',  ( 4.165266963751727225, -2.049631966911998671, -3.550066703508907295 ) ) ;
#18407=CARTESIAN_POINT ( 'NONE',  ( 0.000000000000000000, 0.000000000000000000, -3.499999999999996003 ) ) ;
#18432=DIRECTION ( 'NONE',  ( 1.000000000000000000, 1.479114197289397135E-31, 5.916456789157588541E-31 ) ) ;
#18482=CARTESIAN_POINT ( 'NONE',  ( 5.600000000000000533, 6.472876824008160606E-16, -5.200000000000004619 ) ) ;
#18514=CARTESIAN_POINT ( 'NONE',  ( 4.175326769692853546, -2.060699556489058448, -3.569236330973427407 ) ) ;
#18516=CARTESIAN_POINT ( 'NONE',  ( 4.055498735588670911, -1.410041617599706143, 3.568038744583164057 ) ) ;
#18531=EDGE_LOOP ( 'NONE', ( #20328, #5923, #12749, #21692, #14650, #1505, #5824 ) ) ;
#18556=EDGE_CURVE ( 'NONE', #9771, #3527, #8678, .T. ) ;
#18639=SURFACE_STYLE_FILL_AREA ( #20413 ) ;
#18646=ADVANCED_FACE ( 'NONE', ( #2457 ), #21110, .F. ) ;
#18649=CARTESIAN_POINT ( 'NONE',  ( 4.082498951862915781, -2.020725942163708488, 3.500000000000004885 ) ) ;
#18687=CARTESIAN_POINT ( 'NONE',  ( 3.878096787214418750, 2.680238624821010163, -2.357690525401503923 ) ) ;
#18719=CARTESIAN_POINT ( 'NONE',  ( 0.3126073911696447549, 4.041451884327362798, -2.081668171172168513E-14 ) ) ;
#18777=CARTESIAN_POINT ( 'NONE',  ( 4.151274195509681242, 2.039912954708690052, 3.533232880573531798 ) ) ;
#18786=ORIENTED_EDGE ( 'NONE', *, *, #14672, .T. ) ;
#18788=DIRECTION ( 'NONE',  ( 1.000000000000000000, 1.479114197289397135E-31, 5.916456789157588541E-31 ) ) ;
#18791=ORIENTED_EDGE ( 'NONE', *, *, #16304, .F. ) ;
#18800=ORIENTED_EDGE ( 'NONE', *, *, #11939, .T. ) ;
#18915=FACE_OUTER_BOUND ( 'NONE', #11341, .T. ) ;
#18927=CARTESIAN_POINT ( 'NONE',  ( 4.033901012036328559, 2.321269032827576684, 2.979444097106367817 ) ) ;
#18958=CARTESIAN_POINT ( 'NONE',  ( 0.2174200650117315003, 3.876582599186173095, 0.2855619784720343501 ) ) ;
#18968=CIRCLE ( 'NONE', #21977, 3.500000000000004441 ) ;
#19013=CARTESIAN_POINT ( 'NONE',  ( 4.124214193018063135, 2.028338413290941666, 3.513185186763571721 ) ) ;
#19024=ADVANCED_FACE ( 'NONE', ( #7729 ), #7288, .T. ) ;
#19032=ORIENTED_EDGE ( 'NONE', *, *, #12401, .F. ) ;
#19038=CARTESIAN_POINT ( 'NONE',  ( 0.2174200650117711076, -2.185595227304893307, 3.214438021527944667 ) ) ;
#19097=CARTESIAN_POINT ( 'NONE',  ( 4.180345472528530948, 2.086001522971435485, 3.570468649087180424 ) ) ;
#19104=ORIENTED_EDGE ( 'NONE', *, *, #488, .T. ) ;
#19113=CARTESIAN_POINT ( 'NONE',  ( 0.2175679805409919676, -1.691499766303336649, 3.499999999999960032 ) ) ;
#19130=CARTESIAN_POINT ( 'NONE',  ( 3.973110223768751226, -0.6864646529411689846, -3.565797985667510606 ) ) ;
#19131=FACE_OUTER_BOUND ( 'NONE', #12619, .T. ) ;
#19148=CARTESIAN_POINT ( 'NONE',  ( 4.180231891692593571, 2.049421325483134826, 3.591231015387239545 ) ) ;
#19201=DIRECTION ( 'NONE',  ( 0.000000000000000000, 3.382522293539643228E-32, 1.000000000000000000 ) ) ;
#19224=FACE_OUTER_BOUND ( 'NONE', #10594, .T. ) ;
#19227=CARTESIAN_POINT ( 'NONE',  ( 0.1381419387168374702, -1.355287006802384342, 3.499999999999959588 ) ) ;
#19259=CARTESIAN_POINT ( 'NONE',  ( 3.880206590543155531, 2.665671387532511982, 2.382921720510903452 ) ) ;
#19269=ADVANCED_FACE ( 'NONE', ( #8311 ), #4652, .T. ) ;
#19339=ORIENTED_EDGE ( 'NONE', *, *, #12401, .T. ) ;
#19344=EDGE_CURVE ( 'NONE', #12739, #16509, #4273, .T. ) ;
#19409=CARTESIAN_POINT ( 'NONE',  ( 4.170895651974852569, 2.054890354522450835, -3.559174498016476562 ) ) ;
#19410=CARTESIAN_POINT ( 'NONE',  ( 4.086376042167605860, -1.979461949354230255, 3.571471332069165339 ) ) ;
#19422=ORIENTED_EDGE ( 'NONE', *, *, #19344, .F. ) ;
#19456=EDGE_CURVE ( 'NONE', #13386, #8317, #7900, .T. ) ;
#19460=EDGE_CURVE ( 'NONE', #1004, #19811, #11198, .T. ) ;
#19490=ORIENTED_EDGE ( 'NONE', *, *, #16005, .T. ) ;
#19528=CARTESIAN_POINT ( 'NONE',  ( 0.2182387239012278379, 1.693823289460844927, 3.499999999999957812 ) ) ;
#19605=ORIENTED_EDGE ( 'NONE', *, *, #2470, .F. ) ;
#19625=CARTESIAN_POINT ( 'NONE',  ( 3.973514160553476948, -3.435084588004225115, 1.181876024140334325 ) ) ;
#19630=PLANE ( 'NONE',  #17018 ) ;
#19631=ORIENTED_EDGE ( 'NONE', *, *, #3222, .T. ) ;
#19652=DIRECTION ( 'NONE',  ( -1.000000000000000000, -1.479114197289397135E-31, -5.916456789157588541E-31 ) ) ;
#19662=VERTEX_POINT ( 'NONE', #12484 ) ;
#19705=PLANE ( 'NONE',  #2032 ) ;
#19718=ADVANCED_FACE ( 'NONE', ( #8976 ), #21227, .F. ) ;
#19723=AXIS2_PLACEMENT_3D ( 'NONE', #7474, #21827, #2285 ) ;
#19755=CARTESIAN_POINT ( 'NONE',  ( 5.600000000000000533, 0.000000000000000000, -3.469446951953614189E-15 ) ) ;
#19757=DIRECTION ( 'NONE',  ( -1.725633230170960916E-31, -1.000000000000000000, -2.220446049250310616E-16 ) ) ;
#19759=ADVANCED_FACE ( 'NONE', ( #12839 ), #14839, .F. ) ;
#19771=B_SPLINE_CURVE_WITH_KNOTS ( 'NONE', 3,
 ( #3364, #19113, #19227, #10524, #17690, #3467 ),
 .UNSPECIFIED., .F., .F.,
 ( 4, 2, 4 ),
 ( 0.003805860999069573050, 0.004828937044845143384, 0.005852013090620712850 ),
 .UNSPECIFIED. ) ;
#19772=CARTESIAN_POINT ( 'NONE',  ( 4.114405500665263560, 2.025575754679722618, -3.508400121684928319 ) ) ;
#19773=CARTESIAN_POINT ( 'NONE',  ( 3.948103430091023380, -2.682758828852069843, 2.353325403973813401 ) ) ;
#19783=EDGE_LOOP ( 'NONE', ( #22150, #15851, #13758, #9135 ) ) ;
#19811=VERTEX_POINT ( 'NONE', #6373 ) ;
#19821=CARTESIAN_POINT ( 'NONE',  ( 4.104070371397483541, -2.023683613428375772, -3.505122836902536232 ) ) ;
#19835=EDGE_LOOP ( 'NONE', ( #2825, #123, #20304, #7683 ) ) ;
#19844=CARTESIAN_POINT ( 'NONE',  ( 4.175813232069149450, -2.061359961916378492, -3.570380186727402538 ) ) ;
#19854=B_SPLINE_CURVE_WITH_KNOTS ( 'NONE', 3,
 ( #1592, #1930, #9119, #23258 ),
 .UNSPECIFIED., .F., .F.,
 ( 4, 4 ),
 ( 2.380739283250810230E-07, 0.002044882221487500686 ),
 .UNSPECIFIED. ) ;
#19861=CARTESIAN_POINT ( 'NONE',  ( 4.175813232069142344, -2.061359961916364725, 3.570380186727402538 ) ) ;
#19873=CARTESIAN_POINT ( 'NONE',  ( 3.948103430091032706, -3.379418997639192401, -1.146674596025634152 ) ) ;
#19874=CARTESIAN_POINT ( 'NONE',  ( 0.3126073911696378160, 2.020725942163612121, 3.499999999999975131 ) ) ;
#19880=APPLICATION_CONTEXT ( 'automotive_design' ) ;
#19883=CARTESIAN_POINT ( 'NONE',  ( 4.071447262713884463, 2.020725942163681399, 3.499999999999996003 ) ) ;
#19889=CIRCLE ( 'NONE', #4088, 3.500000000000004441 ) ;
#19892=EDGE_LOOP ( 'NONE', ( #3211, #7196, #16027 ) ) ;
#19936=ORIENTED_EDGE ( 'NONE', *, *, #13389, .F. ) ;
#19949=EDGE_LOOP ( 'NONE', ( #8415, #2966, #3318, #4056 ) ) ;
#19951=( NAMED_UNIT ( * ) PLANE_ANGLE_UNIT ( ) SI_UNIT ( $, .RADIAN. ) );
#19983=CARTESIAN_POINT ( 'NONE',  ( 3.961551342853102398, -2.319461885623262276, -2.982574167881092642 ) ) ;
#19984=DIRECTION ( 'NONE',  ( 0.000000000000000000, -3.382522293539642133E-32, -1.000000000000000000 ) ) ;
#19993=CARTESIAN_POINT ( 'NONE',  ( 4.086376042167607636, 1.979461949354216932, -3.571471332069190652 ) ) ;
#20004=CONICAL_SURFACE ( 'NONE', #20777, 3.500000000000004441, 1.047197551196600296 ) ;
#20015=B_SPLINE_CURVE_WITH_KNOTS ( 'NONE', 3,
 ( #15611, #4684, #13960, #23036, #19038, #1049 ),
 .UNSPECIFIED., .F., .F.,
 ( 4, 2, 4 ),
 ( 0.002044882221487581784, 0.003063384235218523204, 0.004081886248949465057 ),
 .UNSPECIFIED. ) ;
#20020=EDGE_CURVE ( 'NONE', #21815, #9771, #14237, .T. ) ;
#20096=CARTESIAN_POINT ( 'NONE',  ( 3.958476099524783187, -1.406653531810735158, -3.500000000000010214 ) ) ;
#20103=CARTESIAN_POINT ( 'NONE',  ( 3.958484000407251457, -3.734437307742051182, -0.5317648453101290196 ) ) ;
#20144=B_SPLINE_CURVE_WITH_KNOTS ( 'NONE', 3,
 ( #10533, #15813, #80, #21132, #5124 ),
 .UNSPECIFIED., .F., .F.,
 ( 4, 1, 4 ),
 ( 0.000000000000000000, 0.002020725942163687904, 0.004041451884327375808 ),
 .UNSPECIFIED. ) ;
#20171=CARTESIAN_POINT ( 'NONE',  ( 0.3126073911696447549, 2.020725942163625888, -3.499999999999996003 ) ) ;
#20224=VECTOR ( 'NONE', #10892, 1000.000000000000000 ) ;
#20245=PRODUCT_CONTEXT ( 'NONE', #19880, 'mechanical' ) ;
#20255=CARTESIAN_POINT ( 'NONE',  ( 4.114405500665264448, 4.051151509359390168, 6.940203675128279408E-15 ) ) ;
#20294=CARTESIAN_POINT ( 'NONE',  ( 2.036182501904611954E-14, 0.3423821193476729863, -3.500000000000035527 ) ) ;
#20304=ORIENTED_EDGE ( 'NONE', *, *, #1744, .F. ) ;
#20306=EDGE_CURVE ( 'NONE', #12739, #6667, #6971, .T. ) ;
#20311=CARTESIAN_POINT ( 'NONE',  ( 4.175813232069149450, -4.122719923832729449, 0.000000000000000000 ) ) ;
#20324=CARTESIAN_POINT ( 'NONE',  ( 3.950233766685289361, 0.7256672287178125291, -3.499999999999854339 ) ) ;
#20328=ORIENTED_EDGE ( 'NONE', *, *, #2470, .T. ) ;
#20360=CARTESIAN_POINT ( 'NONE',  ( 4.158413352280808439, 4.089743253945565371, 3.469446951953614189E-15 ) ) ;
#20365=CIRCLE ( 'NONE', #1217, 3.500000000000004441 ) ;
#20373=AXIS2_PLACEMENT_3D ( 'NONE', #14891, #10175, #2774 ) ;
#20382=VERTEX_POINT ( 'NONE', #6928 ) ;
#20405=CARTESIAN_POINT ( 'NONE',  ( 3.950250160040463143, -0.7258013381037465850, 3.499999999999968914 ) ) ;
#20407=FACE_OUTER_BOUND ( 'NONE', #9216, .T. ) ;
#20413=FILL_AREA_STYLE ('',( #9241 ) ) ;
#20422=EDGE_LOOP ( 'NONE', ( #5340, #11777, #19490 ) ) ;
#20430=CARTESIAN_POINT ( 'NONE',  ( 4.175813232069142344, 2.061359961916322980, 3.570380186727409200 ) ) ;
#20445=EDGE_LOOP ( 'NONE', ( #22792, #1212, #13437 ) ) ;
#20472=CARTESIAN_POINT ( 'NONE',  ( 3.880206590543188838, 3.396506438958500240, -1.117078279489074788 ) ) ;
#20478=ORIENTED_EDGE ( 'NONE', *, *, #11939, .F. ) ;
#20489=CARTESIAN_POINT ( 'NONE',  ( 4.175813232069149450, 4.122719923832687705, 1.040834085586084257E-14 ) ) ;
#20504=CARTESIAN_POINT ( 'NONE',  ( 0.3126073911696447549, -4.041451884327432076, 3.469446951953614189E-15 ) ) ;
#20518=CARTESIAN_POINT ( 'NONE',  ( 3.951447005078448260, 2.357513599190977249, 2.916666666666662078 ) ) ;
#20525=FACE_OUTER_BOUND ( 'NONE', #18002, .T. ) ;
#20570=AXIS2_PLACEMENT_3D ( 'NONE', #994, #4269, #17315 ) ;
#20575=CARTESIAN_POINT ( 'NONE',  ( 3.948103430090987853, 3.379418997638731881, 1.146674596025563320 ) ) ;
#20664=DIRECTION ( 'NONE',  ( -1.000000000000000000, -1.479114197289397135E-31, -5.916456789157588541E-31 ) ) ;
#20713=DIRECTION ( 'NONE',  ( 7.395570986446975166E-31, 3.382522293539642133E-32, 1.000000000000000000 ) ) ;
#20733=EDGE_CURVE ( 'NONE', #3527, #7132, #10181, .T. ) ;
#20777=AXIS2_PLACEMENT_3D ( 'NONE', #4555, #4315, #7977 ) ;
#20835=AXIS2_PLACEMENT_3D ( 'NONE', #5803, #5904, #7670 ) ;
#20887=ORIENTED_EDGE ( 'NONE', *, *, #12856, .T. ) ;
#20889=CARTESIAN_POINT ( 'NONE',  ( 4.175572532730924991, -2.061029303918041400, 3.569807470274398487 ) ) ;
#20901=DIRECTION ( 'NONE',  ( 7.395570986446975166E-31, 3.382522293539642133E-32, 1.000000000000000000 ) ) ;
#20923=LINE ( 'NONE', #15144, #13989 ) ;
#20924=CARTESIAN_POINT ( 'NONE',  ( 0.3126073911696447549, 4.041451884327362798, -2.081668171172168513E-14 ) ) ;
#20929=CARTESIAN_POINT ( 'NONE',  ( 3.974175853609996700, 2.726149789692757341, 2.409821656223200215 ) ) ;
#20932=DIRECTION ( 'NONE',  ( 1.000000000000000000, 1.479114197289397135E-31, 5.916456789157588541E-31 ) ) ;
#20975=FACE_OUTER_BOUND ( 'NONE', #20445, .T. ) ;
#20985=CARTESIAN_POINT ( 'NONE',  ( 4.158921784487734641, 2.089935040870096294, 3.499999999999967581 ) ) ;
#21042=DIRECTION ( 'NONE',  ( 0.000000000000000000, -3.382522293539642681E-32, -1.000000000000000000 ) ) ;
#21049=EDGE_CURVE ( 'NONE', #1571, #15429, #10405, .T. ) ;
#21068=CARTESIAN_POINT ( 'NONE',  ( 3.951447005078456254, -1.347150628109151427, -3.500000000000006661 ) ) ;
#21110=( BOUNDED_SURFACE ( )  B_SPLINE_SURFACE ( 3, 2, ( 
 ( #22228, #11050, #16340 ),
 ( #16788, #6114, #13288 ),
 ( #20472, #11505, #13053 ),
 ( #18687, #11279, #243 ),
 ( #2107, #12815, #5769 ),
 ( #19993, #16451, #360 ) ),
 .UNSPECIFIED., .F., .F., .T. ) 
 B_SPLINE_SURFACE_WITH_KNOTS ( ( 4, 2, 4 ),
 ( 3, 3 ),
 ( 0.01651999345535504898, 0.01858032176739834312, 0.02064065007944164074 ),
 ( 0.000000000000000000, 1.000000000000000000 ),
 .UNSPECIFIED. ) 
 GEOMETRIC_REPRESENTATION_ITEM ( )  RATIONAL_B_SPLINE_SURFACE ( (
 ( 1.000000000000000000, 0.8047781103519392465, 1.000000000000000000),
 ( 1.000000000000000000, 0.8123785825605738253, 1.000000000000000000),
 ( 1.000000000000000000, 0.8190671539786428257, 1.000000000000000000),
 ( 1.000000000000000000, 0.8192352254836726688, 1.000000000000000000),
 ( 1.000000000000000000, 0.8126129677210214286, 1.000000000000000000),
 ( 1.000000000000000000, 0.8047712537969733404, 1.000000000000000000) ) ) 
 REPRESENTATION_ITEM ( '' )  SURFACE ( )  );
#21112=ORIENTED_EDGE ( 'NONE', *, *, #6250, .F. ) ;
#21132=CARTESIAN_POINT ( 'NONE',  ( 3.951447005078449148, 2.357513599190909304, -2.916666666666663410 ) ) ;
#21227=PLANE ( 'NONE',  #22328 ) ;
#21258=DIRECTION ( 'NONE',  ( -1.000000000000000000, -1.479114197289397135E-31, -5.916456789157588541E-31 ) ) ;
#21285=CARTESIAN_POINT ( 'NONE',  ( 4.050823680195225762, -3.779313952391382792, 0.5899027668435080640 ) ) ;
#21329=CARTESIAN_POINT ( 'NONE',  ( 5.600000000000000533, -4.041451884327432076, -6.938893903907228378E-15 ) ) ;
#21330=( NAMED_UNIT ( * ) PLANE_ANGLE_UNIT ( ) SI_UNIT ( $, .RADIAN. ) );
#21351=CONICAL_SURFACE ( 'NONE', #13442, 3.500000000000004441, 1.047197551196600296 ) ;
#21356=ORIENTED_EDGE ( 'NONE', *, *, #19456, .T. ) ;
#21393=MECHANICAL_DESIGN_GEOMETRIC_PRESENTATION_REPRESENTATION('',(#338),#9722);
#21401=( BOUNDED_SURFACE ( )  B_SPLINE_SURFACE ( 3, 2, ( 
 ( #3755, #18011, #5430 ),
 ( #10706, #23194, #17891 ),
 ( #10923, #12587, #14476 ),
 ( #1873, #19773, #9059 ),
 ( #12223, #16101, #5067 ),
 ( #19410, #8712, #15868 ) ),
 .UNSPECIFIED., .F., .F., .T. ) 
 B_SPLINE_SURFACE_WITH_KNOTS ( ( 4, 2, 4 ),
 ( 3, 3 ),
 ( 0.01651999345535502470, 0.01858032176739832578, 0.02064065007944162686 ),
 ( 0.000000000000000000, 1.000000000000000000 ),
 .UNSPECIFIED. ) 
 GEOMETRIC_REPRESENTATION_ITEM ( )  RATIONAL_B_SPLINE_SURFACE ( (
 ( 1.000000000000000000, 0.8047781103519390244, 1.000000000000000000),
 ( 1.000000000000000000, 0.8123785825604251665, 1.000000000000000000),
 ( 1.000000000000000000, 0.8190671539788410005, 1.000000000000000000),
 ( 1.000000000000000000, 0.8192352254834731617, 1.000000000000000000),
 ( 1.000000000000000000, 0.8126129677211720859, 1.000000000000000000),
 ( 1.000000000000000000, 0.8047712537969733404, 1.000000000000000000) ) ) 
 REPRESENTATION_ITEM ( '' )  SURFACE ( )  );
#21446=ORIENTED_EDGE ( 'NONE', *, *, #3077, .F. ) ;
#21524=CARTESIAN_POINT ( 'NONE',  ( 3.972709601346605890, -2.746729940827227434, 2.374099244652743135 ) ) ;
#21531=PLANE ( 'NONE',  #9166 ) ;
#21540=CARTESIAN_POINT ( 'NONE',  ( 0.03027795056223035047, 0.6888063905604809856, 3.499999999999959144 ) ) ;
#21546=CARTESIAN_POINT ( 'NONE',  ( 4.151274195509685683, 2.039912954708771320, -3.533232880573506485 ) ) ;
#21599=CARTESIAN_POINT ( 'NONE',  ( 4.151274195509683906, -2.039912954708747783, -3.533232880573497159 ) ) ;
#21620=ORIENTED_EDGE ( 'NONE', *, *, #11370, .F. ) ;
#21672=VERTEX_POINT ( 'NONE', #7251 ) ;
#21692=ORIENTED_EDGE ( 'NONE', *, *, #3222, .F. ) ;
#21753=ORIENTED_EDGE ( 'NONE', *, *, #12427, .T. ) ;
#21812=ORIENTED_EDGE ( 'NONE', *, *, #1485, .F. ) ;
#21815=VERTEX_POINT ( 'NONE', #5484 ) ;
#21827=DIRECTION ( 'NONE',  ( -3.944304526105059027E-31, -6.383782391594650107E-16, -1.000000000000000000 ) ) ;
#21844=CARTESIAN_POINT ( 'NONE',  ( 25.15499999999999403, 3.061616997868413710E-16, -2.500000000000007550 ) ) ;
#21867=CARTESIAN_POINT ( 'NONE',  ( 3.973514160553471619, 3.435084588004206019, -1.181876024140340986 ) ) ;
#21875=CARTESIAN_POINT ( 'NONE',  ( 3.951447005078449148, 1.347150628109116566, 3.499999999999997335 ) ) ;
#21909=CONICAL_SURFACE ( 'NONE', #9132, 2.055000000000002380, 0.7853981633974400633 ) ;
#21964=CARTESIAN_POINT ( 'NONE',  ( 4.093692494532777282, -4.043567292011544190, 3.733480660068263491E-17 ) ) ;
#21977=AXIS2_PLACEMENT_3D ( 'NONE', #12601, #14830, #3771 ) ;
#21978=CARTESIAN_POINT ( 'NONE',  ( 3.972073812946708582, -0.6951863858492013382, -3.565770933504613271 ) ) ;
#21979=B_SPLINE_CURVE_WITH_KNOTS ( 'NONE', 3,
 ( #11325, #14413, #2282, #188, #9349, #20171 ),
 .UNSPECIFIED., .F., .F.,
 ( 4, 2, 4 ),
 ( 0.002044882221487541018, 0.003063384235218496315, 0.004081886248949452047 ),
 .UNSPECIFIED. ) ;
#22049=CARTESIAN_POINT ( 'NONE',  ( 4.071447262713891568, -2.020725942163709377, -3.499999999999999556 ) ) ;
#22060=SHAPE_REPRESENTATION_RELATIONSHIP ( 'NONE' , 'NONE' ,  #4439, #11971 ) ;
#22076=CIRCLE ( 'NONE', #20570, 0.4999999999999978351 ) ;
#22090=CARTESIAN_POINT ( 'NONE',  ( 4.180232103119976728, 2.085387772176682919, -3.570466442734708590 ) ) ;
#22096=VERTEX_POINT ( 'NONE', #14386 ) ;
#22115=AXIS2_PLACEMENT_3D ( 'NONE', #4943, #2963, #5306 ) ;
#22116=CARTESIAN_POINT ( 'NONE',  ( 0.3126073911696447549, 2.020725942163625888, -3.499999999999996003 ) ) ;
#22126=CARTESIAN_POINT ( 'NONE',  ( 4.104070371397483541, 4.047367226856696476, 6.938893903907228378E-15 ) ) ;
#22150=ORIENTED_EDGE ( 'NONE', *, *, #21049, .T. ) ;
#22170=CARTESIAN_POINT ( 'NONE',  ( 0.03027795055835478741, 0.6888063905328364323, -3.500000000000034639 ) ) ;
#22218=CARTESIAN_POINT ( 'NONE',  ( 4.175813232069142344, -2.061359961916364725, 3.570380186727402538 ) ) ;
#22220=DIRECTION ( 'NONE',  ( 0.000000000000000000, 3.382522293539642133E-32, 1.000000000000000000 ) ) ;
#22228=CARTESIAN_POINT ( 'NONE',  ( 4.086262629614032527, 4.082406995609999534, 0.07093633357109276061 ) ) ;
#22283=EDGE_CURVE ( 'NONE', #927, #17692, #14812, .T. ) ;
#22307=CARTESIAN_POINT ( 'NONE',  ( 4.082498951862917558, -4.041451884327432076, 1.040834085586084257E-14 ) ) ;
#22310=CARTESIAN_POINT ( 'NONE',  ( 4.132952817037856441, 2.031684012687259955, 3.518979934899767237 ) ) ;
#22328=AXIS2_PLACEMENT_3D ( 'NONE', #12372, #17668, #45 ) ;
#22336=FACE_OUTER_BOUND ( 'NONE', #19892, .T. ) ;
#22382=ADVANCED_FACE ( 'NONE', ( #9159 ), #6853, .F. ) ;
#22394=CARTESIAN_POINT ( 'NONE',  ( 0.000000000000000000, -3.031088913245536087, -1.750000000000001554 ) ) ;
#22421=CARTESIAN_POINT ( 'NONE',  ( 4.175075985190096262, 2.060370777630132544, 3.568666869285558541 ) ) ;
#22452=CARTESIAN_POINT ( 'NONE',  ( 4.052424581287485950, 3.786734753434564560, 0.5771415817954285155 ) ) ;
#22510=SURFACE_STYLE_USAGE ( .BOTH. , #15319 ) ;
#22521=B_SPLINE_CURVE_WITH_KNOTS ( 'NONE', 3,
 ( #5390, #12548, #3614, #97, #7268, #14440 ),
 .UNSPECIFIED., .F., .F.,
 ( 4, 2, 4 ),
 ( 0.000000000000000000, 0.002086519881787258016, 0.004173039763574516031 ),
 .UNSPECIFIED. ) ;
#22580=ADVANCED_FACE ( 'NONE', ( #19131 ), #1403, .T. ) ;
#22586=DIRECTION ( 'NONE',  ( -1.000000000000000000, -1.479114197289397135E-31, -5.916456789157588541E-31 ) ) ;
#22658=CARTESIAN_POINT ( 'NONE',  ( 0.000000000000000000, 3.031088913245536087, 1.749999999999998002 ) ) ;
#22659=CARTESIAN_POINT ( 'NONE',  ( 4.071447262713884463, 2.020725942163681399, 3.499999999999996003 ) ) ;
#22732=UNCERTAINTY_MEASURE_WITH_UNIT (LENGTH_MEASURE( 1.000000000000000082E-05 ), #4279, 'distance_accuracy_value', 'NONE');
#22734=EDGE_CURVE ( 'NONE', #6728, #4783, #5259, .T. ) ;
#22767=AXIS2_PLACEMENT_3D ( 'NONE', #2857, #17196, #19201 ) ;
#22771=CARTESIAN_POINT ( 'NONE',  ( 0.1381419387119531828, -1.355287006778843173, -3.500000000000035527 ) ) ;
#22792=ORIENTED_EDGE ( 'NONE', *, *, #4025, .T. ) ;
#22803=DIRECTION ( 'NONE',  ( -3.944304526105059903E-31, -0.5000000000000014433, -0.8660254037844378194 ) ) ;
#22823=DIRECTION ( 'NONE',  ( 1.000000000000000000, 1.479114197289397135E-31, 5.916456789157588541E-31 ) ) ;
#22829=ORIENTED_EDGE ( 'NONE', *, *, #2342, .T. ) ;
#22853=ORIENTED_EDGE ( 'NONE', *, *, #7627, .T. ) ;
#22957=CARTESIAN_POINT ( 'NONE',  ( 3.806834918298617865, -1.387778780781445676E-14, 3.499999999999940936 ) ) ;
#22958=CARTESIAN_POINT ( 'NONE',  ( 3.973110223767149840, -2.262799480050941678E-11, -3.565797985667468417 ) ) ;
#22977=DIRECTION ( 'NONE',  ( 0.000000000000000000, 3.382522293539642681E-32, 1.000000000000000000 ) ) ;
#22998=DIRECTION ( 'NONE',  ( -3.944304526105060779E-31, -0.8660254037844379305, -0.5000000000000012212 ) ) ;
#23029=CARTESIAN_POINT ( 'NONE',  ( 25.15499999999999403, 8.456305733849119291E-32, 2.499999999999996891 ) ) ;
#23036=CARTESIAN_POINT ( 'NONE',  ( 0.1388410611046271281, -2.351840044243068917, 2.926493552096038897 ) ) ;
#23050=LINE ( 'NONE', #6804, #11913 ) ;
#23062=( GEOMETRIC_REPRESENTATION_CONTEXT ( 3 ) GLOBAL_UNCERTAINTY_ASSIGNED_CONTEXT ( ( #16595 ) ) GLOBAL_UNIT_ASSIGNED_CONTEXT ( ( #15433, #21330, #13906 ) ) REPRESENTATION_CONTEXT ( 'NONE', 'WORKASPACE' ) );
#23068=DIRECTION ( 'NONE',  ( -5.916456789157588541E-31, 3.382522293539642681E-32, 1.000000000000000000 ) ) ;
#23113=VECTOR ( 'NONE', #13905, 1000.000000000000000 ) ;
#23166=AXIS2_PLACEMENT_3D ( 'NONE', #1749, #8700, #23068 ) ;
#23173=CARTESIAN_POINT ( 'NONE',  ( 4.086262841041386373, 2.102637316508701559, -3.500000000000009326 ) ) ;
#23179=EDGE_CURVE ( 'NONE', #17819, #6667, #9192, .T. ) ;
#23194=CARTESIAN_POINT ( 'NONE',  ( 4.033901012036468892, -3.740908793663292098, 0.5205559028931424637 ) ) ;
#23234=PRODUCT ( 'hex flange bolt small_iso_ISO 4162 - M5 x 20 x 20-N', 'hex flange bolt small_iso_ISO 4162 - M5 x 20 x 20-N', '', ( #20245 ) ) ;
#23258=CARTESIAN_POINT ( 'NONE',  ( 0.000000000000000000, -3.031088913245536087, -1.750000000000001554 ) ) ;
ENDSEC;
END-ISO-10303-21;
